ISO-10303-21;
HEADER;
FILE_DESCRIPTION (('STEP AP214'),
    '1' );
FILE_NAME ('Snap Open Cable Crossbars 9.step',
    '2026-10-08T22:59:04',
    ( '' ),
    ( '' ),
    'SwSTEP 2.0',
    'SolidWorks 2020',
    '' );
FILE_SCHEMA (( 'AUTOMOTIVE_DESIGN' ));
ENDSEC;

DATA;
#77=LINE ( 'NONE', #43075, #147484 ) ;
#268=CARTESIAN_POINT ( 'NONE',  ( 21.72449340488910252, 43.99894805634765760, -234.9941606142489832 ) ) ;
#333=B_SPLINE_CURVE_WITH_KNOTS ( 'NONE', 3,
 ( #148170, #229008, #126030, #184720, #50334, #66064, #49068, #145593, #90750, #205561, #47767, #209424, #226401 ),
 .UNSPECIFIED., .F., .F.,
 ( 4, 3, 3, 3, 4 ),
 ( -3.224855718292275407E-06, 0.000000000000000000, 6.199515528651840239E-06, 4.034952380126954614E-05, 7.452715123699161213E-05 ),
 .UNSPECIFIED. ) ;
#428=CARTESIAN_POINT ( 'NONE',  ( 13.99999999999999822, 47.91805600923871822, -233.7139610577891631 ) ) ;
#467=CARTESIAN_POINT ( 'NONE',  ( -12.25000000000000178, 47.91805600923872532, -233.7139610577891631 ) ) ;
#526=ORIENTED_EDGE ( 'NONE', *, *, #181331, .T. ) ;
#913=LINE ( 'NONE', #177050, #202210 ) ;
#978=CARTESIAN_POINT ( 'NONE',  ( -15.69373346032659100, 48.53477651487867206, -233.9781183031096816 ) ) ;
#1185=EDGE_CURVE ( 'NONE', #42318, #28415, #156424, .T. ) ;
#1242=ORIENTED_EDGE ( 'NONE', *, *, #189634, .F. ) ;
#1488=CARTESIAN_POINT ( 'NONE',  ( -18.40000000000000213, 43.39957528361355799, -233.6562381667159798 ) ) ;
#1715=LINE ( 'NONE', #186804, #167998 ) ;
#1919=CARTESIAN_POINT ( 'NONE',  ( 12.42718393586866021, 48.82205200898362563, -233.8342296612539997 ) ) ;
#2279=DIRECTION ( 'NONE',  ( -1.020425574104004394E-15, 0.9126074666063769270, 0.4088369013363280513 ) ) ;
#2285=VERTEX_POINT ( 'NONE', #107231 ) ;
#2310=UNCERTAINTY_MEASURE_WITH_UNIT (LENGTH_MEASURE( 1.000000000000000082E-05 ), #192241, 'distance_accuracy_value', 'NONE');
#2352=DIRECTION ( 'NONE',  ( -1.000000000000000000, -0.000000000000000000, -0.000000000000000000 ) ) ;
#2360=CARTESIAN_POINT ( 'NONE',  ( -16.94275863009466576, 44.08128092168011136, -235.2799346461642358 ) ) ;
#2386=ORIENTED_EDGE ( 'NONE', *, *, #191303, .F. ) ;
#2425=AXIS2_PLACEMENT_3D ( 'NONE', #153513, #135160, #16531 ) ;
#2582=ORIENTED_EDGE ( 'NONE', *, *, #162361, .T. ) ;
#2625=VERTEX_POINT ( 'NONE', #229171 ) ;
#2862=( BOUNDED_CURVE ( )  B_SPLINE_CURVE ( 3, ( #150191, #245435, #48500, #189310 ),
 .UNSPECIFIED., .F., .F. ) 
 B_SPLINE_CURVE_WITH_KNOTS ( ( 4, 4 ),
 ( 5.733388419619901200, 5.983100554402348337 ),
 .UNSPECIFIED. ) 
 CURVE ( )  GEOMETRIC_REPRESENTATION_ITEM ( )  RATIONAL_B_SPLINE_CURVE ( ( 1.000000000000000000, 0.9948104011409416580, 0.9948104011409416580, 1.000000000000000000 ) ) 
 REPRESENTATION_ITEM ( '' )  );
#2964=EDGE_CURVE ( 'NONE', #32681, #8019, #244549, .T. ) ;
#3133=DIRECTION ( 'NONE',  ( 0.2834754621636358940, -0.7201664435733010627, -0.6332471523047666917 ) ) ;
#3202=EDGE_CURVE ( 'NONE', #8358, #150070, #56109, .T. ) ;
#3794=EDGE_CURVE ( 'NONE', #51518, #244889, #127241, .T. ) ;
#4031=CARTESIAN_POINT ( 'NONE',  ( 20.73486653747088937, 41.93205750249717312, -238.6967134976849820 ) ) ;
#4163=CARTESIAN_POINT ( 'NONE',  ( -16.97683809663753252, 44.70268985058793731, -235.0448293460806894 ) ) ;
#4277=CARTESIAN_POINT ( 'NONE',  ( -16.87683809663752399, 39.52051071501344381, -224.9973737707144892 ) ) ;
#4332=SURFACE_SIDE_STYLE ('',( #183004 ) ) ;
#4382=PLANE ( 'NONE',  #204321 ) ;
#4625=ORIENTED_EDGE ( 'NONE', *, *, #59939, .F. ) ;
#4882=CARTESIAN_POINT ( 'NONE',  ( -16.93710578446435733, 44.38079422868823087, -235.1890346188039018 ) ) ;
#4971=DIRECTION ( 'NONE',  ( -0.000000000000000000, 0.9126074666063770380, 0.4088369013363281068 ) ) ;
#5364=DIRECTION ( 'NONE',  ( -0.000000000000000000, 0.9126074666063770380, 0.4088369013363281068 ) ) ;
#5484=CARTESIAN_POINT ( 'NONE',  ( -16.77683809663752257, 51.61886293219124155, -231.9464690156495692 ) ) ;
#5724=DIRECTION ( 'NONE',  ( 1.186688945009010077E-16, 0.4088369013363281623, -0.9126074666063771490 ) ) ;
#5924=DIRECTION ( 'NONE',  ( 1.186688945009010077E-16, 0.4088369013363281068, -0.9126074666063770380 ) ) ;
#5932=ADVANCED_FACE ( 'NONE', ( #55943 ), #75561, .F. ) ;
#5965=ORIENTED_EDGE ( 'NONE', *, *, #2964, .F. ) ;
#5987=CARTESIAN_POINT ( 'NONE',  ( 20.05000000000002913, 52.72272256579930882, -234.4105091754867658 ) ) ;
#6167=CARTESIAN_POINT ( 'NONE',  ( -16.94107738177414291, 51.68386028857256065, -231.8469600742508021 ) ) ;
#6412=DIRECTION ( 'NONE',  ( 1.000000000000000000, -9.792504721693619684E-16, -4.386921467590155985E-16 ) ) ;
#6461=LINE ( 'NONE', #100409, #198078 ) ;
#6528=CARTESIAN_POINT ( 'NONE',  ( -21.65000000000000213, 42.13647595316535188, -239.1530172309881834 ) ) ;
#6999=DIRECTION ( 'NONE',  ( 0.000000000000000000, -0.9126074666063770380, -0.4088369013363281068 ) ) ;
#7080=DIRECTION ( 'NONE',  ( 0.000000000000000000, -0.1207987311150348075, 0.9926770202643947494 ) ) ;
#7217=ORIENTED_EDGE ( 'NONE', *, *, #95506, .F. ) ;
#7237=VERTEX_POINT ( 'NONE', #254503 ) ;
#7298=FACE_OUTER_BOUND ( 'NONE', #47441, .T. ) ;
#7511=CARTESIAN_POINT ( 'NONE',  ( -16.93658623642890859, 44.08829270366707220, -235.2867806363773866 ) ) ;
#7625=CARTESIAN_POINT ( 'NONE',  ( 23.04999999999999716, 44.59642007000408626, -236.3278401793003809 ) ) ;
#7707=CARTESIAN_POINT ( 'NONE',  ( 20.99999999999999645, 44.21724908628621620, -235.4814530999287285 ) ) ;
#7733=EDGE_LOOP ( 'NONE', ( #7217, #208355, #59627, #19637, #88786, #256835, #173776, #129682, #205641, #128064, #129112, #127908 ) ) ;
#7798=DIRECTION ( 'NONE',  ( 0.000000000000000000, -0.4088369013363281068, 0.9126074666063770380 ) ) ;
#7886=ORIENTED_EDGE ( 'NONE', *, *, #244775, .T. ) ;
#8019=VERTEX_POINT ( 'NONE', #56975 ) ;
#8073=CARTESIAN_POINT ( 'NONE',  ( -18.39999999999999858, 40.47920047438133651, -235.2678785906695396 ) ) ;
#8203=ORIENTED_EDGE ( 'NONE', *, *, #1185, .T. ) ;
#8340=EDGE_CURVE ( 'NONE', #143787, #240784, #109903, .T. ) ;
#8358=VERTEX_POINT ( 'NONE', #25591 ) ;
#8395=EDGE_LOOP ( 'NONE', ( #36790, #181896, #232032, #158705 ) ) ;
#8470=ORIENTED_EDGE ( 'NONE', *, *, #46537, .T. ) ;
#8517=CARTESIAN_POINT ( 'NONE',  ( 18.39999999999999503, 43.39957528361355799, -233.6562381667159798 ) ) ;
#8754=CARTESIAN_POINT ( 'NONE',  ( -17.27223548806215447, 52.62863847120288341, -231.0608408311660753 ) ) ;
#8770=CARTESIAN_POINT ( 'NONE',  ( -16.84793658983368303, 44.21181828874585307, -235.2647337580439739 ) ) ;
#8850=DIRECTION ( 'NONE',  ( -0.000000000000000000, 0.9126074666063770380, 0.4088369013363281068 ) ) ;
#8993=CARTESIAN_POINT ( 'NONE',  ( -16.89268316805465986, 51.62340874627276577, -231.9425458505251072 ) ) ;
#9065=EDGE_CURVE ( 'NONE', #144497, #238714, #185645, .T. ) ;
#9254=ORIENTED_EDGE ( 'NONE', *, *, #132070, .T. ) ;
#9430=ORIENTED_EDGE ( 'NONE', *, *, #112083, .T. ) ;
#9505=CARTESIAN_POINT ( 'NONE',  ( -18.40000000000000213, 43.39957528361355799, -233.6562381667159798 ) ) ;
#9644=CARTESIAN_POINT ( 'NONE',  ( -18.44085059012131822, 40.40203773622608452, -235.2576840484422291 ) ) ;
#9794=DIRECTION ( 'NONE',  ( -1.020425574104004394E-15, -0.9126074666063770380, -0.4088369013363281068 ) ) ;
#10031=CARTESIAN_POINT ( 'NONE',  ( -17.22767730083556970, 52.63511723856208846, -231.0537232253000752 ) ) ;
#10174=ORIENTED_EDGE ( 'NONE', *, *, #3794, .F. ) ;
#10197=CARTESIAN_POINT ( 'NONE',  ( -18.34374000495059676, 54.09900352584866567, -229.1663746252470446 ) ) ;
#10226=LINE ( 'NONE', #154884, #121532 ) ;
#10265=EDGE_LOOP ( 'NONE', ( #226611, #68304, #10174, #13735 ) ) ;
#10279=ORIENTED_EDGE ( 'NONE', *, *, #59939, .T. ) ;
#10945=CARTESIAN_POINT ( 'NONE',  ( -17.80356949364745489, 41.60004162723406296, -235.4193010670205979 ) ) ;
#10969=DIRECTION ( 'NONE',  ( 0.000000000000000000, 0.9126074666063770380, 0.4088369013363281068 ) ) ;
#10985=ADVANCED_FACE ( 'NONE', ( #7298 ), #26003, .T. ) ;
#10997=DIRECTION ( 'NONE',  ( -1.073024830501117923E-15, -0.9126074666063771490, -0.4088369013363281623 ) ) ;
#11154=CARTESIAN_POINT ( 'NONE',  ( -17.11825945287481332, 51.52760218553060412, -231.9873527057832234 ) ) ;
#11335=CARTESIAN_POINT ( 'NONE',  ( -16.84981964351489125, 44.34925329055300836, -235.2389759867866417 ) ) ;
#11336=EDGE_LOOP ( 'NONE', ( #112706, #8203, #144502, #111341, #218854, #64929, #153358, #145469, #85290, #153751 ) ) ;
#11521=CARTESIAN_POINT ( 'NONE',  ( -16.86379686415369861, 44.04906952004396459, -235.3100105550803960 ) ) ;
#11685=AXIS2_PLACEMENT_3D ( 'NONE', #112015, #110710, #170743 ) ;
#11686=FACE_OUTER_BOUND ( 'NONE', #26406, .T. ) ;
#11791=ORIENTED_EDGE ( 'NONE', *, *, #182521, .F. ) ;
#11812=DIRECTION ( 'NONE',  ( 0.000000000000000000, 0.4088369013363281068, -0.9126074666063770380 ) ) ;
#11875=CARTESIAN_POINT ( 'NONE',  ( -18.40000000000000213, 43.47495547423554996, -233.9258172596817076 ) ) ;
#12010=DIRECTION ( 'NONE',  ( 1.000000000000000000, -4.851622311275597861E-17, 1.082981191754466620E-16 ) ) ;
#12028=VERTEX_POINT ( 'NONE', #41368 ) ;
#12250=EDGE_CURVE ( 'NONE', #159544, #162125, #183424, .T. ) ;
#12252=ORIENTED_EDGE ( 'NONE', *, *, #240226, .F. ) ;
#12558=CARTESIAN_POINT ( 'NONE',  ( -16.87331047859649757, 51.61886293219124155, -231.9464690156495692 ) ) ;
#12628=CARTESIAN_POINT ( 'NONE',  ( -16.93440969289731157, 44.06337821721247394, -235.2817209114844275 ) ) ;
#12871=( BOUNDED_SURFACE ( )  B_SPLINE_SURFACE ( 3, 2, ( 
 ( #198280, #40540, #97867 ),
 ( #140888, #239991, #116205 ),
 ( #159189, #156634, #254380 ),
 ( #19662, #178766, #155344 ) ),
 .UNSPECIFIED., .F., .F., .F. ) 
 B_SPLINE_SURFACE_WITH_KNOTS ( ( 4, 4 ),
 ( 3, 3 ),
 ( 0.0008258556059633782300, 0.0009616864997632838244 ),
 ( 0.000000000000000000, 1.000000000000000000 ),
 .UNSPECIFIED. ) 
 GEOMETRIC_REPRESENTATION_ITEM ( )  RATIONAL_B_SPLINE_SURFACE ( (
 ( 1.000000000000000000, 0.9152888060719127639, 1.000000000000000000),
 ( 1.000000000000000000, 0.9327727094137693298, 1.000000000000000000),
 ( 1.000000000000000000, 0.9369023509258749272, 1.000000000000000000),
 ( 1.000000000000000000, 0.9246339933864399230, 1.000000000000000000) ) ) 
 REPRESENTATION_ITEM ( '' )  SURFACE ( )  );
#12997=AXIS2_PLACEMENT_3D ( 'NONE', #56075, #15725, #39128 ) ;
#13027=LINE ( 'NONE', #252885, #49526 ) ;
#13032=CARTESIAN_POINT ( 'NONE',  ( -16.93589915522259304, 51.67754058831158659, -231.8559428553618318 ) ) ;
#13111=VERTEX_POINT ( 'NONE', #58342 ) ;
#13247=ORIENTED_EDGE ( 'NONE', *, *, #190321, .T. ) ;
#13334=EDGE_CURVE ( 'NONE', #212682, #162878, #333, .T. ) ;
#13487=ORIENTED_EDGE ( 'NONE', *, *, #185958, .T. ) ;
#13518=EDGE_CURVE ( 'NONE', #75024, #172022, #99582, .T. ) ;
#13735=ORIENTED_EDGE ( 'NONE', *, *, #241866, .F. ) ;
#13792=LINE ( 'NONE', #78578, #124757 ) ;
#13836=CARTESIAN_POINT ( 'NONE',  ( -16.87683809663752399, 51.08978195134977796, -232.2756554297758953 ) ) ;
#13897=CARTESIAN_POINT ( 'NONE',  ( -16.93970660449832621, 44.02061140864920930, -235.2815329157306508 ) ) ;
#13902=CARTESIAN_POINT ( 'NONE',  ( -21.65000000000000213, 44.22674245267958781, -235.2580479164738279 ) ) ;
#13997=DIRECTION ( 'NONE',  ( 1.186688945009010077E-16, 0.4088369013363281068, -0.9126074666063770380 ) ) ;
#14084=DIRECTION ( 'NONE',  ( -1.000000000000000000, -0.000000000000000000, 0.000000000000000000 ) ) ;
#14090=ORIENTED_EDGE ( 'NONE', *, *, #88674, .T. ) ;
#14642=ADVANCED_FACE ( 'NONE', ( #217138 ), #84750, .F. ) ;
#14789=VERTEX_POINT ( 'NONE', #114872 ) ;
#14805=VERTEX_POINT ( 'NONE', #247953 ) ;
#14906=ADVANCED_FACE ( 'NONE', ( #220405 ), #77021, .F. ) ;
#15124=CARTESIAN_POINT ( 'NONE',  ( -16.97683810757273193, 51.05890824306432307, -232.1973218175039051 ) ) ;
#15401=CYLINDRICAL_SURFACE ( 'NONE', #181384, 0.1000000000000024342 ) ;
#15437=FACE_OUTER_BOUND ( 'NONE', #24588, .T. ) ;
#15514=CARTESIAN_POINT ( 'NONE',  ( -16.78055652883087134, 44.14664813320825232, -235.2974609155759254 ) ) ;
#15523=ORIENTED_EDGE ( 'NONE', *, *, #203737, .F. ) ;
#15606=CARTESIAN_POINT ( 'NONE',  ( -16.94132844910801339, 51.64367728818032788, -231.8888519332613214 ) ) ;
#15689=STYLED_ITEM ( 'NONE', ( #249642 ), #21402 ) ;
#15725=DIRECTION ( 'NONE',  ( 0.7071067811865494601, -0.2890913453342123240, 0.6453109281988432810 ) ) ;
#15821=EDGE_CURVE ( 'NONE', #108079, #107188, #184482, .T. ) ;
#16139=AXIS2_PLACEMENT_3D ( 'NONE', #56560, #236507, #197380 ) ;
#16213=FACE_OUTER_BOUND ( 'NONE', #45792, .T. ) ;
#16314=CARTESIAN_POINT ( 'NONE',  ( 12.60053434924910754, 47.12508421510193557, -234.5737628866445164 ) ) ;
#16531=DIRECTION ( 'NONE',  ( 1.000000000000000000, 0.000000000000000000, 0.000000000000000000 ) ) ;
#16588=VECTOR ( 'NONE', #48631, 1000.000000000000000 ) ;
#16655=( BOUNDED_CURVE ( )  B_SPLINE_CURVE ( 3, ( #170939, #32705, #250412, #112217 ),
 .UNSPECIFIED., .F., .F. ) 
 B_SPLINE_CURVE_WITH_KNOTS ( ( 4, 4 ),
 ( 4.712388980384686121, 5.672655318024754756 ),
 .UNSPECIFIED. ) 
 CURVE ( )  GEOMETRIC_REPRESENTATION_ITEM ( )  RATIONAL_B_SPLINE_CURVE ( ( 1.000000000000000000, 0.9246222802177250788, 0.9246222802177250788, 1.000000000000000000 ) ) 
 REPRESENTATION_ITEM ( '' )  );
#16716=CARTESIAN_POINT ( 'NONE',  ( -14.77738660682463312, 46.65242889160100503, -234.7339858363278040 ) ) ;
#16743=CIRCLE ( 'NONE', #224823, 0.9000000000000014655 ) ;
#16793=CARTESIAN_POINT ( 'NONE',  ( -16.78569801330233702, 44.14263524120624282, -235.2979910463945714 ) ) ;
#16884=LINE ( 'NONE', #70463, #257848 ) ;
#16986=CARTESIAN_POINT ( 'NONE',  ( -21.65000000000000213, 42.13647595316535188, -239.1530172309881834 ) ) ;
#17046=LINE ( 'NONE', #39186, #33899 ) ;
#17275=CARTESIAN_POINT ( 'NONE',  ( 23.24999999999999645, 45.89348038176515843, -239.2231437130149061 ) ) ;
#17666=CARTESIAN_POINT ( 'NONE',  ( -16.93710578446435022, 51.37355040952256502, -232.0563660034529221 ) ) ;
#17735=CARTESIAN_POINT ( 'NONE',  ( 18.39999999999999503, 43.39957528361355799, -233.6562381667159798 ) ) ;
#17970=CARTESIAN_POINT ( 'NONE',  ( -12.25000000000000178, 48.12247445990688988, -234.1702647910923361 ) ) ;
#18048=CARTESIAN_POINT ( 'NONE',  ( -16.79184697841823493, 44.13976825150989214, -235.2983682103465526 ) ) ;
#18286=LINE ( 'NONE', #116120, #36908 ) ;
#18333=B_SPLINE_CURVE_WITH_KNOTS ( 'NONE', 3,
 ( #238143, #139011, #218572, #199034, #20410, #99892, #179488, #242002, #64647, #180757 ),
 .UNSPECIFIED., .F., .F.,
 ( 4, 3, 3, 4 ),
 ( 1.953076773942978418E-15, 8.145022132834464008E-06, 1.905645951092501956E-05, 2.061107371225841053E-05 ),
 .UNSPECIFIED. ) ;
#18422=ORIENTED_EDGE ( 'NONE', *, *, #236081, .T. ) ;
#18687=ORIENTED_EDGE ( 'NONE', *, *, #13334, .T. ) ;
#18851=ORIENTED_EDGE ( 'NONE', *, *, #146752, .F. ) ;
#19348=CARTESIAN_POINT ( 'NONE',  ( -21.65000000000000213, 44.13548170601895038, -235.2989316066074821 ) ) ;
#19629=EDGE_CURVE ( 'NONE', #251476, #79207, #87950, .T. ) ;
#19637=ORIENTED_EDGE ( 'NONE', *, *, #182180, .T. ) ;
#19662=CARTESIAN_POINT ( 'NONE',  ( -16.94878442675511820, 44.08354183875889731, -235.2764748885172708 ) ) ;
#19744=( BOUNDED_CURVE ( )  B_SPLINE_CURVE ( 3, ( #116095, #131791, #11875, #34021 ),
 .UNSPECIFIED., .F., .F. ) 
 B_SPLINE_CURVE_WITH_KNOTS ( ( 4, 4 ),
 ( 1.570796326794916320, 3.141592653589837969 ),
 .UNSPECIFIED. ) 
 CURVE ( )  GEOMETRIC_REPRESENTATION_ITEM ( )  RATIONAL_B_SPLINE_CURVE ( ( 1.000000000000000000, 0.8047378541243590533, 0.8047378541243590533, 1.000000000000000000 ) ) 
 REPRESENTATION_ITEM ( '' )  );
#19765=DIRECTION ( 'NONE',  ( -1.000000000000000000, 0.000000000000000000, 0.000000000000000000 ) ) ;
#19773=VERTEX_POINT ( 'NONE', #203921 ) ;
#19828=ORIENTED_EDGE ( 'NONE', *, *, #162361, .F. ) ;
#20236=CARTESIAN_POINT ( 'NONE',  ( 14.45963434102923806, 49.63592998410994284, -233.3809899335355453 ) ) ;
#20272=EDGE_CURVE ( 'NONE', #134853, #77934, #78020, .T. ) ;
#20286=CARTESIAN_POINT ( 'NONE',  ( -17.04295772865519965, 51.58824128325588987, -231.8781152409123933 ) ) ;
#20410=CARTESIAN_POINT ( 'NONE',  ( -16.88219499860498019, 44.13476732972441852, -235.2990254453784189 ) ) ;
#20560=B_SPLINE_CURVE_WITH_KNOTS ( 'NONE', 3,
 ( #202376, #4163, #244056, #245364, #164545, #101956, #66722, #84957, #125416, #141129 ),
 .UNSPECIFIED., .F., .F.,
 ( 4, 2, 2, 2, 4 ),
 ( 0.000000000000000000, 0.0003916577441626381485, 0.0005874866162439739466, 0.0006854010522846671347, 0.0007833154883253604312 ),
 .UNSPECIFIED. ) ;
#20606=CARTESIAN_POINT ( 'NONE',  ( -14.45422546970484667, 49.62720671425053354, -233.3859273903071312 ) ) ;
#20720=FACE_OUTER_BOUND ( 'NONE', #190278, .T. ) ;
#21121=LINE ( 'NONE', #26245, #124234 ) ;
#21175=EDGE_CURVE ( 'NONE', #159477, #144497, #172127, .T. ) ;
#21193=EDGE_LOOP ( 'NONE', ( #142905, #255327, #156686, #117802 ) ) ;
#21251=AXIS2_PLACEMENT_3D ( 'NONE', #65841, #146644, #102369 ) ;
#21339=VECTOR ( 'NONE', #196594, 1000.000000000000000 ) ;
#21402=MANIFOLD_SOLID_BREP ( 'Stock-MAS-200-1', #111536 ) ;
#21489=EDGE_CURVE ( 'NONE', #28415, #134853, #141240, .T. ) ;
#21760=ADVANCED_FACE ( 'NONE', ( #90227 ), #151537, .F. ) ;
#21861=AXIS2_PLACEMENT_3D ( 'NONE', #88221, #247316, #111666 ) ;
#21873=CARTESIAN_POINT ( 'NONE',  ( -16.27683809663751191, 41.27791846035903234, -237.2365415511148115 ) ) ;
#21906=CARTESIAN_POINT ( 'NONE',  ( -15.55912972643741199, 44.73202778202335139, -236.6305442897015610 ) ) ;
#22012=ORIENTED_EDGE ( 'NONE', *, *, #143911, .F. ) ;
#22040=DIRECTION ( 'NONE',  ( 0.000000000000000000, -0.9126074666063769270, -0.4088369013363280513 ) ) ;
#22331=LINE ( 'NONE', #164391, #31280 ) ;
#22496=B_SPLINE_CURVE_WITH_KNOTS ( 'NONE', 3,
 ( #232960, #107849, #231672, #129963, #191272, #92138, #112995, #12628, #247354, #227792, #153449, #54283, #171714, #249935, #251197, #72600, #13897, #252483, #93413 ),
 .UNSPECIFIED., .F., .F.,
 ( 4, 3, 3, 3, 3, 3, 4 ),
 ( 0.0001624081864585792971, 0.0001685232196531718575, 0.0001764526673566863891, 0.0001916878551483168600, 0.0002009890782182536747, 0.0002238845907555072430, 0.0002283406619926262157 ),
 .UNSPECIFIED. ) ;
#22699=ORIENTED_EDGE ( 'NONE', *, *, #137075, .T. ) ;
#22714=LINE ( 'NONE', #44818, #116096 ) ;
#22819=CARTESIAN_POINT ( 'NONE',  ( 12.93279065517211457, 49.36478519392532149, -233.5395520442455961 ) ) ;
#22838=CARTESIAN_POINT ( 'NONE',  ( -16.89268316805465986, 51.62340874627276577, -231.9425458505251072 ) ) ;
#23039=ORIENTED_EDGE ( 'NONE', *, *, #26354, .F. ) ;
#23257=CARTESIAN_POINT ( 'NONE',  ( -16.90257928357875272, 44.12128666712435177, -235.3007907132581522 ) ) ;
#23260=CARTESIAN_POINT ( 'NONE',  ( -23.25000000000000355, 41.03261631955726330, -236.6889770711509584 ) ) ;
#23475=AXIS2_PLACEMENT_3D ( 'NONE', #45695, #103080, #203494 ) ;
#23970=CARTESIAN_POINT ( 'NONE',  ( -20.65000000000000568, 45.89348038176515843, -239.2231437130149061 ) ) ;
#24076=ORIENTED_EDGE ( 'NONE', *, *, #103688, .F. ) ;
#24515=EDGE_CURVE ( 'NONE', #244889, #109657, #76932, .T. ) ;
#24588=EDGE_LOOP ( 'NONE', ( #62027, #181013, #233855, #208870 ) ) ;
#24632=CARTESIAN_POINT ( 'NONE',  ( -18.40000000000000213, 53.98582189624753624, -228.9137301112145622 ) ) ;
#24846=EDGE_LOOP ( 'NONE', ( #160640, #23039, #104951, #127790, #218200, #28777, #194708, #108388, #150183, #46639, #14090, #237592, #40136, #86424 ) ) ;
#25011=CIRCLE ( 'NONE', #195883, 0.1999999999999987899 ) ;
#25042=( BOUNDED_CURVE ( )  B_SPLINE_CURVE ( 3, ( #246374, #26054, #185114, #145974 ),
 .UNSPECIFIED., .F., .F. ) 
 B_SPLINE_CURVE_WITH_KNOTS ( ( 4, 4 ),
 ( 3.752122642744639691, 4.712388980384671022 ),
 .UNSPECIFIED. ) 
 CURVE ( )  GEOMETRIC_REPRESENTATION_ITEM ( )  RATIONAL_B_SPLINE_CURVE ( ( 1.000000000000000000, 0.9246222802177307409, 0.9246222802177307409, 1.000000000000000000 ) ) 
 REPRESENTATION_ITEM ( '' )  );
#25111=ORIENTED_EDGE ( 'NONE', *, *, #236449, .T. ) ;
#25263=LINE ( 'NONE', #65645, #37774 ) ;
#25591=CARTESIAN_POINT ( 'NONE',  ( -16.97683809663752186, 44.82209472663103611, -234.9913374327310578 ) ) ;
#25775=CARTESIAN_POINT ( 'NONE',  ( -18.40000000000000213, 54.02969457822032950, -229.1974241798695004 ) ) ;
#25794=DIRECTION ( 'NONE',  ( 0.000000000000000000, 0.9126074666063769270, 0.4088369013363280513 ) ) ;
#26003=TOROIDAL_SURFACE ( 'NONE', #121867, 14.20833333333334103, 0.1000000000000000056 ) ;
#26054=CARTESIAN_POINT ( 'NONE',  ( -16.98495255085917321, 51.61018462143365326, -231.8894715066228116 ) ) ;
#26245=CARTESIAN_POINT ( 'NONE',  ( -18.40000000000000213, 55.18266668263805030, -231.5853321237989633 ) ) ;
#26354=EDGE_CURVE ( 'NONE', #108079, #57171, #59574, .T. ) ;
#26406=EDGE_LOOP ( 'NONE', ( #239318, #526, #68548, #50027, #44718, #196489, #115273, #79757, #215176 ) ) ;
#26553=AXIS2_PLACEMENT_3D ( 'NONE', #117547, #60127, #100516 ) ;
#26655=ORIENTED_EDGE ( 'NONE', *, *, #65177, .F. ) ;
#26694=EDGE_CURVE ( 'NONE', #152864, #246882, #143282, .T. ) ;
#26806=ORIENTED_EDGE ( 'NONE', *, *, #24515, .T. ) ;
#26850=AXIS2_PLACEMENT_3D ( 'NONE', #138068, #79377, #241053 ) ;
#26983=ADVANCED_FACE ( 'NONE', ( #253343 ), #58969, .F. ) ;
#27095=CARTESIAN_POINT ( 'NONE',  ( -16.80468759584941196, 44.17521108926469964, -235.2897310320125825 ) ) ;
#27108=CARTESIAN_POINT ( 'NONE',  ( 15.48841904831874849, 52.18649987366221410, -233.2135506059238139 ) ) ;
#27849=FACE_OUTER_BOUND ( 'NONE', #100418, .T. ) ;
#28153=DIRECTION ( 'NONE',  ( -0.000000000000000000, 0.9126074666063770380, 0.4088369013363281068 ) ) ;
#28182=CARTESIAN_POINT ( 'NONE',  ( -16.92507428761700083, 51.56100593717672353, -231.9723882365938152 ) ) ;
#28216=CARTESIAN_POINT ( 'NONE',  ( -16.87036670365548474, 51.72098459467785858, -231.8575261499355236 ) ) ;
#28328=EDGE_LOOP ( 'NONE', ( #164592, #208017, #75831, #10279 ) ) ;
#28369=CARTESIAN_POINT ( 'NONE',  ( -16.85697194749148409, 44.41252758811717882, -235.2202446609966842 ) ) ;
#28415=VERTEX_POINT ( 'NONE', #36631 ) ;
#28451=CYLINDRICAL_SURFACE ( 'NONE', #39050, 0.5000000000000004441 ) ;
#28596=EDGE_CURVE ( 'NONE', #109657, #201957, #191846, .T. ) ;
#28777=ORIENTED_EDGE ( 'NONE', *, *, #248678, .F. ) ;
#28967=ORIENTED_EDGE ( 'NONE', *, *, #220656, .T. ) ;
#29691=CIRCLE ( 'NONE', #108775, 1.749999999999999778 ) ;
#29757=CARTESIAN_POINT ( 'NONE',  ( 20.73486653747088937, 45.03492288895885309, -237.3066680331414489 ) ) ;
#29817=ORIENTED_EDGE ( 'NONE', *, *, #137989, .F. ) ;
#29902=ORIENTED_EDGE ( 'NONE', *, *, #38873, .T. ) ;
#30219=ADVANCED_FACE ( 'NONE', ( #109115 ), #118781, .T. ) ;
#30245=ORIENTED_EDGE ( 'NONE', *, *, #217221, .T. ) ;
#30721=CARTESIAN_POINT ( 'NONE',  ( -18.40000000000000213, 56.47972699439914379, -234.4806356575134885 ) ) ;
#30894=ADVANCED_FACE ( 'NONE', ( #238268 ), #15401, .T. ) ;
#30916=EDGE_CURVE ( 'NONE', #156660, #48836, #913, .T. ) ;
#31016=ADVANCED_FACE ( 'NONE', ( #205553 ), #43927, .T. ) ;
#31222=FACE_OUTER_BOUND ( 'NONE', #7733, .T. ) ;
#31280=VECTOR ( 'NONE', #221756, 1000.000000000000114 ) ;
#31334=DIRECTION ( 'NONE',  ( 0.000000000000000000, 0.4088369013363281068, -0.9126074666063770380 ) ) ;
#31564=ORIENTED_EDGE ( 'NONE', *, *, #94110, .T. ) ;
#31585=DIRECTION ( 'NONE',  ( 1.186688945009009831E-16, 0.4088369013363281068, -0.9126074666063770380 ) ) ;
#31614=EDGE_CURVE ( 'NONE', #168251, #47203, #96199, .T. ) ;
#31750=EDGE_LOOP ( 'NONE', ( #136372, #240862, #62064, #221393 ) ) ;
#31978=CARTESIAN_POINT ( 'NONE',  ( -16.93388492042258875, 44.07359652990944454, -235.2844227631439367 ) ) ;
#32277=VERTEX_POINT ( 'NONE', #228387 ) ;
#32285=DIRECTION ( 'NONE',  ( 1.000000000000000000, 0.000000000000000000, 0.000000000000000000 ) ) ;
#32304=VECTOR ( 'NONE', #28153, 1000.000000000000114 ) ;
#32318=DIRECTION ( 'NONE',  ( -1.073024830501117923E-15, 0.9126074666063771490, 0.4088369013363281623 ) ) ;
#32492=CARTESIAN_POINT ( 'NONE',  ( 15.74999999999999645, 48.12247445990688988, -234.1702647910923361 ) ) ;
#32610=CARTESIAN_POINT ( 'NONE',  ( -16.93521499325732549, 51.65267039475685351, -231.8822487893360176 ) ) ;
#32681=VERTEX_POINT ( 'NONE', #166845 ) ;
#32705=CARTESIAN_POINT ( 'NONE',  ( -17.04761207306819060, 44.10422576783453508, -235.2291619687160562 ) ) ;
#33059=CARTESIAN_POINT ( 'NONE',  ( -16.92989507731676113, 51.40668072027212787, -232.0415240324163335 ) ) ;
#33195=SURFACE_SIDE_STYLE ('',( #233917 ) ) ;
#33204=ADVANCED_FACE ( 'NONE', ( #162355 ), #176785, .F. ) ;
#33298=DIRECTION ( 'NONE',  ( 1.000000000000000000, 0.000000000000000000, -0.000000000000000000 ) ) ;
#33330=CARTESIAN_POINT ( 'NONE',  ( 15.15590539855245744, 46.89406695649157797, -234.6540829047534942 ) ) ;
#33780=DIRECTION ( 'NONE',  ( -1.020425574104004394E-15, 0.9126074666063770380, 0.4088369013363281068 ) ) ;
#33788=ORIENTED_EDGE ( 'NONE', *, *, #42579, .T. ) ;
#33899=VECTOR ( 'NONE', #82105, 1000.000000000000227 ) ;
#34021=CARTESIAN_POINT ( 'NONE',  ( -18.40000000000000213, 43.42149616655404287, -233.9497663708821165 ) ) ;
#34137=PLANE ( 'NONE',  #54601 ) ;
#34207=FACE_OUTER_BOUND ( 'NONE', #70794, .T. ) ;
#34353=EDGE_LOOP ( 'NONE', ( #256338, #18422, #192581, #185801, #253173, #107254 ) ) ;
#35178=CARTESIAN_POINT ( 'NONE',  ( -16.93353400591625757, 51.67199383424718206, -231.8628248725454455 ) ) ;
#35348=CARTESIAN_POINT ( 'NONE',  ( -18.34374000495060386, 40.40989152675300033, -235.2989281452919954 ) ) ;
#35406=DIRECTION ( 'NONE',  ( 1.020425574104004394E-15, -0.9126074666063770380, -0.4088369013363281068 ) ) ;
#35499=ORIENTED_EDGE ( 'NONE', *, *, #150943, .T. ) ;
#35605=EDGE_CURVE ( 'NONE', #159477, #245204, #47954, .T. ) ;
#35698=AXIS2_PLACEMENT_3D ( 'NONE', #225552, #229440, #50767 ) ;
#35764=ORIENTED_EDGE ( 'NONE', *, *, #223158, .T. ) ;
#35806=DIRECTION ( 'NONE',  ( -3.035766082959431348E-14, 0.9126074666063771490, 0.4088369013363281623 ) ) ;
#35826=ORIENTED_EDGE ( 'NONE', *, *, #135039, .T. ) ;
#35886=EDGE_CURVE ( 'NONE', #238714, #42318, #18333, .T. ) ;
#36164=ORIENTED_EDGE ( 'NONE', *, *, #143911, .T. ) ;
#36631=CARTESIAN_POINT ( 'NONE',  ( -17.11825945287482753, 44.22674245267958781, -235.2580479164738279 ) ) ;
#36640=ORIENTED_EDGE ( 'NONE', *, *, #62588, .F. ) ;
#36692=VECTOR ( 'NONE', #227135, 1000.000000000000000 ) ;
#36790=ORIENTED_EDGE ( 'NONE', *, *, #189634, .T. ) ;
#36908=VECTOR ( 'NONE', #59957, 1000.000000000000114 ) ;
#36912=CARTESIAN_POINT ( 'NONE',  ( -14.00000000000000178, 47.91805600923872532, -233.7139610577891631 ) ) ;
#36970=CARTESIAN_POINT ( 'NONE',  ( -17.11825945287482753, 44.18585876254595490, -235.1667871698132046 ) ) ;
#37237=AXIS2_PLACEMENT_3D ( 'NONE', #110311, #115442, #209408 ) ;
#37243=CIRCLE ( 'NONE', #112074, 0.5000000000000004441 ) ;
#37267=CARTESIAN_POINT ( 'NONE',  ( -16.88783316861814043, 51.52553600391507160, -231.9882783296907576 ) ) ;
#37288=CARTESIAN_POINT ( 'NONE',  ( -16.95709691156038446, 51.60968432554658847, -231.9505809183468727 ) ) ;
#37564=CARTESIAN_POINT ( 'NONE',  ( -12.93407622233967658, 46.82384836101675063, -234.6777522051880851 ) ) ;
#37599=CARTESIAN_POINT ( 'NONE',  ( -14.77538296656416072, 49.52260852254784140, -233.4480600891349127 ) ) ;
#37724=CYLINDRICAL_SURFACE ( 'NONE', #82987, 0.1000000000000078187 ) ;
#37729=CARTESIAN_POINT ( 'NONE',  ( -16.93294127766158752, 51.67000402742814202, -231.8651761569155099 ) ) ;
#37748=B_SPLINE_CURVE_WITH_KNOTS ( 'NONE', 3,
 ( #58527, #252892, #13032, #194239, #35178, #37729, #196762, #177246, #114674, #211205, #256696, #32610, #53414, #112129, #15606, #132970 ),
 .UNSPECIFIED., .F., .F.,
 ( 4, 3, 3, 3, 3, 4 ),
 ( 0.000000000000000000, 1.810570668010520807E-05, 2.740575833571303106E-05, 4.256816319437020446E-05, 5.213463471026028777E-05, 6.641585710718293713E-05 ),
 .UNSPECIFIED. ) ;
#37774=VECTOR ( 'NONE', #225972, 1000.000000000000000 ) ;
#37907=DIRECTION ( 'NONE',  ( 0.000000000000000000, 0.9126074666063769270, 0.4088369013363280513 ) ) ;
#37917=EDGE_CURVE ( 'NONE', #19773, #125918, #122794, .T. ) ;
#38040=PLANE ( 'NONE',  #26553 ) ;
#38075=CARTESIAN_POINT ( 'NONE',  ( 20.05000000000002913, 45.23934133962702475, -237.7629717664446503 ) ) ;
#38140=DIRECTION ( 'NONE',  ( -0.5932847527679298016, -0.3291107096594085846, 0.7346423231209707749 ) ) ;
#38227=VERTEX_POINT ( 'NONE', #190004 ) ;
#38512=CARTESIAN_POINT ( 'NONE',  ( 13.22461703343585349, 49.52260852254784140, -233.4480600891348558 ) ) ;
#38611=EDGE_CURVE ( 'NONE', #68814, #47203, #179251, .T. ) ;
#38635=DIRECTION ( 'NONE',  ( 0.000000000000000000, -0.4088369013363281068, 0.9126074666063770380 ) ) ;
#38808=DIRECTION ( 'NONE',  ( 0.000000000000000000, -0.9126074666063660468, -0.4088369013363524762 ) ) ;
#38873=EDGE_CURVE ( 'NONE', #183570, #126269, #46123, .T. ) ;
#38998=DIRECTION ( 'NONE',  ( -1.073024830501117923E-15, 0.9126074666063771490, 0.4088369013363281623 ) ) ;
#39050=AXIS2_PLACEMENT_3D ( 'NONE', #4031, #82250, #19765 ) ;
#39128=DIRECTION ( 'NONE',  ( 0.000000000000000000, 0.9126074666063769270, 0.4088369013363280513 ) ) ;
#39186=CARTESIAN_POINT ( 'NONE',  ( 21.72449340488910607, 51.48232928251994167, -231.6416980232910987 ) ) ;
#39228=ORIENTED_EDGE ( 'NONE', *, *, #70550, .F. ) ;
#39323=FACE_OUTER_BOUND ( 'NONE', #194730, .T. ) ;
#39736=AXIS2_PLACEMENT_3D ( 'NONE', #64768, #62217, #41389 ) ;
#39819=CARTESIAN_POINT ( 'NONE',  ( 15.66039659514495774, 48.63331072832806967, -233.9296379114950923 ) ) ;
#39861=CARTESIAN_POINT ( 'NONE',  ( -16.87242674293849376, 51.61985789917108747, -231.9460232827009918 ) ) ;
#39997=CARTESIAN_POINT ( 'NONE',  ( -16.94445028196808778, 44.07934375239701552, -235.2779890399608576 ) ) ;
#40136=ORIENTED_EDGE ( 'NONE', *, *, #74252, .F. ) ;
#40178=CARTESIAN_POINT ( 'NONE',  ( -12.60829076262180237, 49.08016403251640725, -233.6979168753148599 ) ) ;
#40504=VECTOR ( 'NONE', #239338, 1000.000000000000114 ) ;
#40540=CARTESIAN_POINT ( 'NONE',  ( -16.91256925476569606, 44.01351207619228489, -235.3144196755796429 ) ) ;
#40636=PLANE ( 'NONE',  #48998 ) ;
#40937=DIRECTION ( 'NONE',  ( -0.5932847527679310229, -0.3291107096594071413, 0.7346423231209704419 ) ) ;
#40949=CARTESIAN_POINT ( 'NONE',  ( 17.23472005113826810, 52.56455255973604324, -231.1306584961272392 ) ) ;
#40950=EDGE_CURVE ( 'NONE', #211293, #168251, #118385, .T. ) ;
#41284=ORIENTED_EDGE ( 'NONE', *, *, #96264, .F. ) ;
#41368=CARTESIAN_POINT ( 'NONE',  ( 20.09999999999999787, 44.21724908628621620, -235.4814530999287285 ) ) ;
#41389=DIRECTION ( 'NONE',  ( -1.000000000000000000, 0.000000000000000000, 0.000000000000000000 ) ) ;
#41452=CARTESIAN_POINT ( 'NONE',  ( -18.40000000000000213, 40.40436687347765599, -235.2865959907995546 ) ) ;
#41454=CARTESIAN_POINT ( 'NONE',  ( -15.57281606413133801, 48.82205200898362563, -233.8342296612540281 ) ) ;
#41459=ORIENTED_EDGE ( 'NONE', *, *, #226132, .T. ) ;
#41553=EDGE_CURVE ( 'NONE', #213760, #237540, #57449, .T. ) ;
#41562=ORIENTED_EDGE ( 'NONE', *, *, #155188, .F. ) ;
#41740=ORIENTED_EDGE ( 'NONE', *, *, #86351, .T. ) ;
#41842=DIRECTION ( 'NONE',  ( 0.000000000000000000, 0.9126074666063769270, 0.4088369013363280513 ) ) ;
#42127=DIRECTION ( 'NONE',  ( 1.000000000000000000, 0.000000000000000000, 0.000000000000000000 ) ) ;
#42210=CARTESIAN_POINT ( 'NONE',  ( 16.87683809663749557, 51.61886293219124155, -231.9464690156495692 ) ) ;
#42313=DIRECTION ( 'NONE',  ( 1.000000000000000000, 0.000000000000000000, 0.000000000000000000 ) ) ;
#42318=VERTEX_POINT ( 'NONE', #114023 ) ;
#42518=CARTESIAN_POINT ( 'NONE',  ( -17.01764560440450680, 44.22674245196203202, -235.2580479167952774 ) ) ;
#42579=EDGE_CURVE ( 'NONE', #226785, #19773, #91298, .T. ) ;
#42685=CARTESIAN_POINT ( 'NONE',  ( -21.65000000000000213, 45.23934133962703186, -237.7629717664446787 ) ) ;
#42711=CARTESIAN_POINT ( 'NONE',  ( -12.24999999999999822, 48.22810253856973617, -234.1229447132332382 ) ) ;
#42802=ADVANCED_FACE ( 'NONE', ( #61146 ), #164110, .F. ) ;
#42976=ADVANCED_FACE ( 'NONE', ( #226625 ), #167988, .F. ) ;
#43019=CARTESIAN_POINT ( 'NONE',  ( -18.39999999999999858, 40.29670989715187090, -235.0462836312595130 ) ) ;
#43075=CARTESIAN_POINT ( 'NONE',  ( 18.39999999999999147, 41.49355468354239207, -237.7178856438439141 ) ) ;
#43843=LINE ( 'NONE', #148077, #32304 ) ;
#43871=DIRECTION ( 'NONE',  ( -1.186688945009009831E-16, -0.4088369013363280513, 0.9126074666063770380 ) ) ;
#43927=CYLINDRICAL_SURFACE ( 'NONE', #39736, 1.500000000000001332 ) ;
#44061=CARTESIAN_POINT ( 'NONE',  ( -16.78493832629888161, 44.14991418685006153, -235.2970290647050433 ) ) ;
#44353=CARTESIAN_POINT ( 'NONE',  ( -17.11825945287482753, 44.22674245267958781, -235.2580479164738279 ) ) ;
#44588=LINE ( 'NONE', #147532, #257518 ) ;
#44718=ORIENTED_EDGE ( 'NONE', *, *, #111955, .T. ) ;
#44722=AXIS2_PLACEMENT_3D ( 'NONE', #247882, #129227, #208772 ) ;
#44745=DIRECTION ( 'NONE',  ( -1.000000000000000000, -0.000000000000000000, 0.000000000000000000 ) ) ;
#44818=CARTESIAN_POINT ( 'NONE',  ( 12.25000000000000000, 47.91805600923871822, -233.7139610577891631 ) ) ;
#45217=CARTESIAN_POINT ( 'NONE',  ( -18.40000000000000213, 50.88295650978584206, -230.3037755757580953 ) ) ;
#45584=CARTESIAN_POINT ( 'NONE',  ( -16.78805706634180694, 51.61424155150325532, -231.9504541878317809 ) ) ;
#45665=ORIENTED_EDGE ( 'NONE', *, *, #15821, .F. ) ;
#45695=CARTESIAN_POINT ( 'NONE',  ( -23.25000000000000355, 44.18585876254595490, -235.1667871698132046 ) ) ;
#45741=ORIENTED_EDGE ( 'NONE', *, *, #12250, .F. ) ;
#45792=EDGE_LOOP ( 'NONE', ( #35826, #219848, #177981, #219915 ) ) ;
#45904=CARTESIAN_POINT ( 'NONE',  ( -16.94107738177415712, 44.01795756907898749, -235.2811900454759666 ) ) ;
#45963=ORIENTED_EDGE ( 'NONE', *, *, #150682, .F. ) ;
#46123=LINE ( 'NONE', #147814, #159595 ) ;
#46311=CARTESIAN_POINT ( 'NONE',  ( 18.39999999999997371, 40.29670989715187090, -235.0462836312595130 ) ) ;
#46465=CARTESIAN_POINT ( 'NONE',  ( -16.87683809663752399, 44.13548170601895038, -235.2989316066074821 ) ) ;
#46537=EDGE_CURVE ( 'NONE', #42318, #163693, #85565, .T. ) ;
#46547=ORIENTED_EDGE ( 'NONE', *, *, #112083, .F. ) ;
#46573=CARTESIAN_POINT ( 'NONE',  ( -18.44085059012131822, 54.07345485900965087, -229.1330576149768774 ) ) ;
#46585=CARTESIAN_POINT ( 'NONE',  ( -16.87333278164109629, 44.60397586039064066, -235.1628955916846166 ) ) ;
#46599=CARTESIAN_POINT ( 'NONE',  ( -16.87683809663753465, 44.74130085420379999, -235.1207662860264520 ) ) ;
#46616=CARTESIAN_POINT ( 'NONE',  ( -16.91247567987036504, 44.11235215177685376, -235.2993409081199445 ) ) ;
#46639=ORIENTED_EDGE ( 'NONE', *, *, #146606, .F. ) ;
#46661=CARTESIAN_POINT ( 'NONE',  ( -15.55912972643741199, 44.64076703536271395, -236.6714279798352152 ) ) ;
#46737=LINE ( 'NONE', #126279, #190564 ) ;
#46809=PLANE ( 'NONE',  #158982 ) ;
#46888=CARTESIAN_POINT ( 'NONE',  ( -17.01473183483382101, 44.22674245267958781, -235.2580479164738279 ) ) ;
#47203=VERTEX_POINT ( 'NONE', #216806 ) ;
#47441=EDGE_LOOP ( 'NONE', ( #64825, #79544, #112385, #26806 ) ) ;
#47636=CARTESIAN_POINT ( 'NONE',  ( -17.05016517656212116, 44.15619606664471775, -235.2896518282563818 ) ) ;
#47647=STYLED_ITEM ( 'NONE', ( #63027 ), #157027 ) ;
#47723=CARTESIAN_POINT ( 'NONE',  ( -16.86733706339143524, 51.66079883479768853, -231.9101604434227113 ) ) ;
#47767=CARTESIAN_POINT ( 'NONE',  ( -16.90987985657661952, 51.63327247197580760, -231.9314585426081123 ) ) ;
#47954=LINE ( 'NONE', #207048, #207946 ) ;
#47994=CARTESIAN_POINT ( 'NONE',  ( 18.39999999999999503, 45.89348038176515843, -239.2231437130149061 ) ) ;
#48026=AXIS2_PLACEMENT_3D ( 'NONE', #217866, #61386, #140936 ) ;
#48169=CARTESIAN_POINT ( 'NONE',  ( -16.79140778683514057, 51.60243904148639160, -231.9593695168616421 ) ) ;
#48188=CARTESIAN_POINT ( 'NONE',  ( 18.39999999999999503, 45.89348038176515843, -239.2231437130149061 ) ) ;
#48375=LINE ( 'NONE', #92634, #195128 ) ;
#48417=ORIENTED_EDGE ( 'NONE', *, *, #152813, .F. ) ;
#48447=CARTESIAN_POINT ( 'NONE',  ( -18.37160782347004329, 40.40888803190161127, -235.2966881398250507 ) ) ;
#48500=CARTESIAN_POINT ( 'NONE',  ( -17.29158576265543346, 52.57432316029790087, -231.0639701379864448 ) ) ;
#48631=DIRECTION ( 'NONE',  ( -1.000000000000000000, -0.000000000000000000, 0.000000000000000000 ) ) ;
#48836=VERTEX_POINT ( 'NONE', #104284 ) ;
#48998=AXIS2_PLACEMENT_3D ( 'NONE', #103110, #80982, #163126 ) ;
#49068=CARTESIAN_POINT ( 'NONE',  ( -16.93935632781549572, 51.64085851770598623, -231.8985589246740631 ) ) ;
#49171=CARTESIAN_POINT ( 'NONE',  ( -16.87998658237752281, 44.33045077069872519, -235.2115878677316800 ) ) ;
#49252=LINE ( 'NONE', #144479, #130869 ) ;
#49305=CARTESIAN_POINT ( 'NONE',  ( -17.71734398241074260, 53.42160327193604985, -230.1610529824684193 ) ) ;
#49431=CARTESIAN_POINT ( 'NONE',  ( -16.81744102076748959, 51.61886293219124155, -231.9464690156495692 ) ) ;
#49526=VECTOR ( 'NONE', #129101, 1000.000000000000114 ) ;
#49631=CARTESIAN_POINT ( 'NONE',  ( -18.36973785203556275, 54.09804631718828460, -229.1642379400122138 ) ) ;
#50027=ORIENTED_EDGE ( 'NONE', *, *, #232325, .T. ) ;
#50055=AXIS2_PLACEMENT_3D ( 'NONE', #85195, #143915, #142619 ) ;
#50066=DIRECTION ( 'NONE',  ( 0.2834754621636439431, 0.9519569026850353000, 0.1158435055642859091 ) ) ;
#50334=CARTESIAN_POINT ( 'NONE',  ( -16.94165728009537020, 51.64084748583298534, -231.8951239911713174 ) ) ;
#50395=ADVANCED_FACE ( 'NONE', ( #249830 ), #153339, .T. ) ;
#50660=VERTEX_POINT ( 'NONE', #171001 ) ;
#50767=DIRECTION ( 'NONE',  ( -1.000000000000000000, -0.000000000000000000, 0.000000000000000000 ) ) ;
#50847=DIRECTION ( 'NONE',  ( 0.000000000000000000, -0.4088369013363281068, 0.9126074666063770380 ) ) ;
#50858=ORIENTED_EDGE ( 'NONE', *, *, #217086, .T. ) ;
#51518=VERTEX_POINT ( 'NONE', #171650 ) ;
#51827=DIRECTION ( 'NONE',  ( -1.000000000000000000, 0.000000000000000000, 0.000000000000000000 ) ) ;
#51890=CARTESIAN_POINT ( 'NONE',  ( -16.86337532320262156, 44.03295079807835322, -235.3120272856442625 ) ) ;
#52037=ADVANCED_FACE ( 'NONE', ( #160771 ), #240287, .F. ) ;
#52555=CARTESIAN_POINT ( 'NONE',  ( -16.97683809663752186, 50.93224991157930504, -232.2540631895259082 ) ) ;
#52698=( NAMED_UNIT ( * ) PLANE_ANGLE_UNIT ( ) SI_UNIT ( $, .RADIAN. ) );
#52837=CARTESIAN_POINT ( 'NONE',  ( 14.87567385445977486, 46.70278183066207589, -234.7177704364561066 ) ) ;
#53006=VECTOR ( 'NONE', #139980, 1000.000000000000114 ) ;
#53414=CARTESIAN_POINT ( 'NONE',  ( -16.93658211146644987, 51.65037976959903432, -231.8840172928964591 ) ) ;
#53435=CIRCLE ( 'NONE', #186720, 1.500000000000001332 ) ;
#54122=CARTESIAN_POINT ( 'NONE',  ( 14.56326696814972266, 46.56726880910646571, -234.7610735323249571 ) ) ;
#54170=CARTESIAN_POINT ( 'NONE',  ( -23.25000000000000355, 53.37686160793744961, -235.8706811220569932 ) ) ;
#54228=CARTESIAN_POINT ( 'NONE',  ( -16.80070461187981223, 51.62163376436579654, -231.9452277169720560 ) ) ;
#54273=ADVANCED_FACE ( 'NONE', ( #132351 ), #211912, .F. ) ;
#54283=CARTESIAN_POINT ( 'NONE',  ( -16.93230518875208190, 44.04699785180793015, -235.2829609980169892 ) ) ;
#54390=LINE ( 'NONE', #234305, #180433 ) ;
#54469=PLANE ( 'NONE',  #145842 ) ;
#54601=AXIS2_PLACEMENT_3D ( 'NONE', #228464, #191921, #129341 ) ;
#54856=CARTESIAN_POINT ( 'NONE',  ( -16.94107738177414291, 51.68386028857255354, -231.8469600742508021 ) ) ;
#54880=CARTESIAN_POINT ( 'NONE',  ( -18.40000000000000213, 54.09900352584865857, -229.1663746252470446 ) ) ;
#54938=FACE_OUTER_BOUND ( 'NONE', #110524, .T. ) ;
#55363=FACE_OUTER_BOUND ( 'NONE', #58996, .T. ) ;
#55400=DIRECTION ( 'NONE',  ( -0.000000000000000000, 0.9126074666063770380, 0.4088369013363281068 ) ) ;
#55820=ORIENTED_EDGE ( 'NONE', *, *, #197140, .T. ) ;
#55860=DIRECTION ( 'NONE',  ( -0.7071067811865462405, -0.2890913453342134898, 0.6453109281988460566 ) ) ;
#55865=VECTOR ( 'NONE', #10969, 1000.000000000000114 ) ;
#55943=FACE_OUTER_BOUND ( 'NONE', #156474, .T. ) ;
#56075=CARTESIAN_POINT ( 'NONE',  ( -16.27683809663750480, 41.27791846035906786, -237.2365415511148115 ) ) ;
#56109=CIRCLE ( 'NONE', #226826, 0.09999999999999939493 ) ;
#56126=VERTEX_POINT ( 'NONE', #91389 ) ;
#56161=EDGE_LOOP ( 'NONE', ( #133500, #243173, #1242, #130868, #77776 ) ) ;
#56560=CARTESIAN_POINT ( 'NONE',  ( 20.99999999999999645, 41.11438369982452912, -236.8714985644722617 ) ) ;
#56582=LINE ( 'NONE', #198694, #53006 ) ;
#56711=ADVANCED_FACE ( 'NONE', ( #11686 ), #87336, .F. ) ;
#56771=CARTESIAN_POINT ( 'NONE',  ( -16.87333278164162920, 51.20547199152485973, -232.2055066581121991 ) ) ;
#56975=CARTESIAN_POINT ( 'NONE',  ( -15.75000000000000355, 48.12247445990688988, -234.1702647910923361 ) ) ;
#57009=ORIENTED_EDGE ( 'NONE', *, *, #28596, .T. ) ;
#57115=CARTESIAN_POINT ( 'NONE',  ( -15.73854595235692244, 48.33210975535352105, -234.0748017065895681 ) ) ;
#57171=VERTEX_POINT ( 'NONE', #169182 ) ;
#57181=ORIENTED_EDGE ( 'NONE', *, *, #135379, .F. ) ;
#57215=EDGE_LOOP ( 'NONE', ( #159577, #22699, #87044 ) ) ;
#57449=LINE ( 'NONE', #54880, #203943 ) ;
#57489=CARTESIAN_POINT ( 'NONE',  ( -16.97683810757273193, 44.69543639514680677, -235.0480788047526914 ) ) ;
#57552=ORIENTED_EDGE ( 'NONE', *, *, #95506, .T. ) ;
#57826=CARTESIAN_POINT ( 'NONE',  ( -21.65000000000000213, 44.22674245267958781, -235.2580479164738279 ) ) ;
#58038=CARTESIAN_POINT ( 'NONE',  ( 13.77030915526558275, 49.66582466164801701, -233.3627041834999432 ) ) ;
#58067=CARTESIAN_POINT ( 'NONE',  ( -16.77431908686106610, 51.60765445881215641, -231.9560861657696194 ) ) ;
#58342=CARTESIAN_POINT ( 'NONE',  ( 16.87683809663749557, 51.61886293219124155, -231.9464690156495692 ) ) ;
#58527=CARTESIAN_POINT ( 'NONE',  ( -16.94107738177414291, 51.68386028857255354, -231.8469600742508021 ) ) ;
#58570=AXIS2_PLACEMENT_3D ( 'NONE', #36970, #176466, #198564 ) ;
#58740=AXIS2_PLACEMENT_3D ( 'NONE', #136212, #3133, #77528 ) ;
#58969=CYLINDRICAL_SURFACE ( 'NONE', #126720, 1.749999999999999778 ) ;
#58996=EDGE_LOOP ( 'NONE', ( #19828, #222336, #36164, #177293, #236019, #231280, #253436, #126980, #234292, #4625, #101438, #39228, #24076, #155294 ) ) ;
#59307=CARTESIAN_POINT ( 'NONE',  ( 12.48201962039795454, 48.91301996986817358, -233.7868972119375712 ) ) ;
#59392=CARTESIAN_POINT ( 'NONE',  ( -18.34374000495060386, 40.40989152675300033, -235.2989281452919954 ) ) ;
#59574=LINE ( 'NONE', #139110, #197268 ) ;
#59627=ORIENTED_EDGE ( 'NONE', *, *, #104355, .F. ) ;
#59939=EDGE_CURVE ( 'NONE', #14789, #38227, #133635, .T. ) ;
#59957=DIRECTION ( 'NONE',  ( 0.000000000000000000, -0.4088369013363281068, 0.9126074666063770380 ) ) ;
#59981=EDGE_LOOP ( 'NONE', ( #109369, #184219, #167108, #107421 ) ) ;
#60052=DIRECTION ( 'NONE',  ( 0.000000000000000000, 0.4088369013363281068, -0.9126074666063770380 ) ) ;
#60127=DIRECTION ( 'NONE',  ( -1.000000000000000000, 9.312479980434134033E-16, 4.171876297610248080E-16 ) ) ;
#60581=AXIS2_PLACEMENT_3D ( 'NONE', #250055, #71438, #51827 ) ;
#60980=CARTESIAN_POINT ( 'NONE',  ( -18.39999999999999858, 40.45536607095846193, -235.2785561097531968 ) ) ;
#60982=FACE_OUTER_BOUND ( 'NONE', #57215, .T. ) ;
#61069=CIRCLE ( 'NONE', #148580, 0.1000000000000115796 ) ;
#61098=CARTESIAN_POINT ( 'NONE',  ( -16.81744102076748959, 51.61886293219124155, -231.9464690156495692 ) ) ;
#61146=FACE_OUTER_BOUND ( 'NONE', #197061, .T. ) ;
#61333=ORIENTED_EDGE ( 'NONE', *, *, #81052, .F. ) ;
#61386=DIRECTION ( 'NONE',  ( -1.000000000000000000, 4.851622311275599093E-17, -1.082981191754466866E-16 ) ) ;
#61406=ADVANCED_FACE ( 'NONE', ( #15437 ), #217444, .F. ) ;
#61628=VECTOR ( 'NONE', #137370, 1000.000000000000000 ) ;
#61707=DIRECTION ( 'NONE',  ( 1.000000000000000000, 0.000000000000000000, 0.000000000000000000 ) ) ;
#61832=DIRECTION ( 'NONE',  ( -1.073024830501117725E-15, -0.9126074666063770380, -0.4088369013363281068 ) ) ;
#61922=CARTESIAN_POINT ( 'NONE',  ( 13.43663047529820176, 49.59862664907821994, -233.4030665626792995 ) ) ;
#61944=CARTESIAN_POINT ( 'NONE',  ( -16.88328101497759448, 51.61979511467394133, -231.9456647872781900 ) ) ;
#62027=ORIENTED_EDGE ( 'NONE', *, *, #105806, .F. ) ;
#62064=ORIENTED_EDGE ( 'NONE', *, *, #3202, .F. ) ;
#62217=DIRECTION ( 'NONE',  ( -0.000000000000000000, 0.9126074666063769270, 0.4088369013363280513 ) ) ;
#62277=CARTESIAN_POINT ( 'NONE',  ( -15.75000000000001066, 48.22675593180858300, -234.1235479764714853 ) ) ;
#62397=CARTESIAN_POINT ( 'NONE',  ( 20.04999999999999716, 44.62608598762253109, -236.3940605665350745 ) ) ;
#62588=EDGE_CURVE ( 'NONE', #237540, #74012, #149232, .T. ) ;
#62698=CARTESIAN_POINT ( 'NONE',  ( 13.99999999999999822, 47.91805600923871822, -233.7139610577891631 ) ) ;
#63027=PRESENTATION_STYLE_ASSIGNMENT (( #241677 ) ) ;
#63035=CARTESIAN_POINT ( 'NONE',  ( 18.39999999999997371, 54.09900352584866567, -229.1663746252470446 ) ) ;
#63280=VERTEX_POINT ( 'NONE', #227458 ) ;
#63635=FACE_OUTER_BOUND ( 'NONE', #11336, .T. ) ;
#63675=ORIENTED_EDGE ( 'NONE', *, *, #20272, .F. ) ;
#63939=B_SPLINE_CURVE_WITH_KNOTS ( 'NONE', 3,
 ( #111266, #228661, #210371, #95542, #192101, #33059, #154290, #209076, #232516, #52555 ),
 .UNSPECIFIED., .F., .F.,
 ( 4, 2, 2, 2, 4 ),
 ( 5.285415200657074080E-16, 9.930191194499933679E-05, 0.0001986038238894701521, 0.0003972076477784117557, 0.0007944152955563480887 ),
 .UNSPECIFIED. ) ;
#64271=DIRECTION ( 'NONE',  ( 1.000000000000000000, -4.851622311275599710E-17, 1.082981191754467113E-16 ) ) ;
#64274=DIRECTION ( 'NONE',  ( 1.000000000000000000, 0.000000000000000000, 0.000000000000000000 ) ) ;
#64289=VECTOR ( 'NONE', #180870, 1000.000000000000000 ) ;
#64549=( BOUNDED_SURFACE ( )  B_SPLINE_SURFACE ( 3, 2, ( 
 ( #9644, #149180, #130871 ),
 ( #10945, #89172, #248260 ),
 ( #168776, #69636, #228714 ),
 ( #205259, #106153, #170054 ) ),
 .UNSPECIFIED., .F., .F., .T. ) 
 B_SPLINE_SURFACE_WITH_KNOTS ( ( 4, 4 ),
 ( 3, 3 ),
 ( 5.727910411845712702, 5.983100554402348337 ),
 ( 0.000000000000000000, 1.000000000000000000 ),
 .UNSPECIFIED. ) 
 GEOMETRIC_REPRESENTATION_ITEM ( )  RATIONAL_B_SPLINE_SURFACE ( (
 ( 1.000000000000000000, 0.8946697475932871013, 1.000000000000000000),
 ( 1.000000000000000000, 0.9035312726220107171, 1.000000000000000000),
 ( 1.000000000000000000, 0.9104333467450814732, 1.000000000000000000),
 ( 1.000000000000000000, 0.9152888060719538421, 1.000000000000000000) ) ) 
 REPRESENTATION_ITEM ( '' )  SURFACE ( )  );
#64584=ORIENTED_EDGE ( 'NONE', *, *, #223809, .T. ) ;
#64647=CARTESIAN_POINT ( 'NONE',  ( -16.87383368123029825, 44.13548170601895038, -235.2989316066074821 ) ) ;
#64755=VERTEX_POINT ( 'NONE', #243910 ) ;
#64768=CARTESIAN_POINT ( 'NONE',  ( 20.04999999999999716, 41.52322060116084401, -237.7841060310786077 ) ) ;
#64825=ORIENTED_EDGE ( 'NONE', *, *, #85710, .F. ) ;
#64853=ORIENTED_EDGE ( 'NONE', *, *, #13518, .T. ) ;
#64929=ORIENTED_EDGE ( 'NONE', *, *, #8340, .T. ) ;
#65106=CARTESIAN_POINT ( 'NONE',  ( 18.39999999999999503, 50.88295650978584206, -230.3037755757580953 ) ) ;
#65110=ORIENTED_EDGE ( 'NONE', *, *, #178844, .F. ) ;
#65177=EDGE_CURVE ( 'NONE', #68414, #151483, #85783, .T. ) ;
#65294=B_SPLINE_CURVE_WITH_KNOTS ( 'NONE', 3,
 ( #213606, #94941, #153706, #257820, #174549, #134066, #135347, #195364, #16716, #96226, #117091, #98759, #175794, #255252, #194077, #76663, #156242, #178368, #216169, #37564, #196611, #256531, #139186, #79216, #157539, #17970 ),
 .UNSPECIFIED., .F., .F.,
 ( 4, 2, 2, 2, 2, 2, 2, 2, 2, 2, 2, 2, 4 ),
 ( 0.005476422646581359521, 0.006160811967703560058, 0.006845201288825762329, 0.007187395949386863464, 0.007529590609947964600, 0.007871785270509065735, 0.008213979931070168605, 0.008556174591631268006, 0.008898369252192370876, 0.009240563912753472012, 0.009582758573314573147, 0.01026714789443681011, 0.01095153721555904534 ),
 .UNSPECIFIED. ) ;
#65635=ORIENTED_EDGE ( 'NONE', *, *, #153782, .T. ) ;
#65645=CARTESIAN_POINT ( 'NONE',  ( -17.01825945287482966, 44.09459801588531036, -235.2076708599468020 ) ) ;
#65841=CARTESIAN_POINT ( 'NONE',  ( 20.99999999999999645, 51.70063031245850027, -232.1289905089708441 ) ) ;
#66064=CARTESIAN_POINT ( 'NONE',  ( -16.94052228080550648, 51.64087742373390455, -231.8968528649357950 ) ) ;
#66102=CARTESIAN_POINT ( 'NONE',  ( -20.65000000000000568, 53.37686160793744961, -235.8706811220569932 ) ) ;
#66310=CARTESIAN_POINT ( 'NONE',  ( -17.22361732159831860, 52.62473031027478498, -231.0628565205512928 ) ) ;
#66520=EDGE_CURVE ( 'NONE', #38227, #50660, #240424, .T. ) ;
#66543=ORIENTED_EDGE ( 'NONE', *, *, #128489, .T. ) ;
#66667=FACE_OUTER_BOUND ( 'NONE', #212441, .T. ) ;
#66688=ORIENTED_EDGE ( 'NONE', *, *, #113241, .F. ) ;
#66702=ORIENTED_EDGE ( 'NONE', *, *, #26694, .T. ) ;
#66722=CARTESIAN_POINT ( 'NONE',  ( -16.89020380669786903, 44.23350592178142904, -235.2550179656449814 ) ) ;
#67015=ORIENTED_EDGE ( 'NONE', *, *, #196871, .F. ) ;
#67662=DIRECTION ( 'NONE',  ( 1.073024830501117923E-15, -0.9126074666063771490, -0.4088369013363281623 ) ) ;
#67743=CARTESIAN_POINT ( 'NONE',  ( -16.83794479845803949, 51.48839318213948957, -232.0308244825887414 ) ) ;
#67877=VECTOR ( 'NONE', #181683, 999.9999999999998863 ) ;
#68177=ORIENTED_EDGE ( 'NONE', *, *, #223809, .F. ) ;
#68227=DIRECTION ( 'NONE',  ( 1.000000000000000000, 0.000000000000000000, 0.000000000000000000 ) ) ;
#68269=LINE ( 'NONE', #227331, #190940 ) ;
#68304=ORIENTED_EDGE ( 'NONE', *, *, #24515, .F. ) ;
#68414=VERTEX_POINT ( 'NONE', #125126 ) ;
#68548=ORIENTED_EDGE ( 'NONE', *, *, #227211, .T. ) ;
#68747=CARTESIAN_POINT ( 'NONE',  ( -16.77180007708461673, 44.12235304356341459, -235.3048130856369653 ) ) ;
#68788=VERTEX_POINT ( 'NONE', #79229 ) ;
#68795=VERTEX_POINT ( 'NONE', #101326 ) ;
#68814=VERTEX_POINT ( 'NONE', #66102 ) ;
#68892=CARTESIAN_POINT ( 'NONE',  ( -16.87036670365548474, 51.72098459467785858, -231.8575261499355236 ) ) ;
#68986=FACE_OUTER_BOUND ( 'NONE', #69369, .T. ) ;
#69017=CARTESIAN_POINT ( 'NONE',  ( -16.77683809663752257, 51.60783545504968117, -231.9559722212415522 ) ) ;
#69159=APPLICATION_CONTEXT ( 'automotive_design' ) ;
#69225=CARTESIAN_POINT ( 'NONE',  ( -18.34374000495059676, 54.09900352584866567, -229.1663746252470446 ) ) ;
#69236=VERTEX_POINT ( 'NONE', #204021 ) ;
#69369=EDGE_LOOP ( 'NONE', ( #22012, #83508, #45741 ) ) ;
#69394=ORIENTED_EDGE ( 'NONE', *, *, #35605, .T. ) ;
#69636=CARTESIAN_POINT ( 'NONE',  ( -17.27223548805945086, 42.80240007841014460, -235.4628745677799202 ) ) ;
#69710=CARTESIAN_POINT ( 'NONE',  ( 20.73486653747088937, 52.51830411513114427, -233.9542054421835644 ) ) ;
#70032=CARTESIAN_POINT ( 'NONE',  ( -18.41431012584569515, 54.11435837739090715, -229.1438153579562993 ) ) ;
#70133=B_SPLINE_CURVE_WITH_KNOTS ( 'NONE', 3,
 ( #243531, #161451, #140572, #25775 ),
 .UNSPECIFIED., .F., .F.,
 ( 4, 4 ),
 ( 0.000000000000000000, 7.713889350926964386E-05 ),
 .UNSPECIFIED. ) ;
#70311=CARTESIAN_POINT ( 'NONE',  ( -16.79363873026997922, 51.61582291306198300, -231.9490907809428961 ) ) ;
#70338=VECTOR ( 'NONE', #216175, 1000.000000000000000 ) ;
#70463=CARTESIAN_POINT ( 'NONE',  ( 18.39999999999999503, 55.18266668263805030, -231.5853321237989633 ) ) ;
#70544=CARTESIAN_POINT ( 'NONE',  ( 13.99999999999999822, 47.91805600923871822, -233.7139610577891631 ) ) ;
#70550=EDGE_CURVE ( 'NONE', #131243, #248676, #93892, .T. ) ;
#70793=CARTESIAN_POINT ( 'NONE',  ( 20.73486653747088582, 52.72272256579930172, -234.4105091754867658 ) ) ;
#70794=EDGE_LOOP ( 'NONE', ( #2386, #168270, #158662, #211959 ) ) ;
#70894=ORIENTED_EDGE ( 'NONE', *, *, #141754, .F. ) ;
#71169=ORIENTED_EDGE ( 'NONE', *, *, #12250, .T. ) ;
#71226=EDGE_CURVE ( 'NONE', #167295, #181396, #22496, .T. ) ;
#71273=CARTESIAN_POINT ( 'NONE',  ( -16.94445028196807002, 51.64060657411747712, -231.8906364537310196 ) ) ;
#71329=CARTESIAN_POINT ( 'NONE',  ( -16.83558968593869309, 44.14671151211591393, -235.2939007918319021 ) ) ;
#71438=DIRECTION ( 'NONE',  ( 0.000000000000000000, 0.9126074666063771490, 0.4088369013363281623 ) ) ;
#71605=DIRECTION ( 'NONE',  ( -1.000000000000000000, 0.000000000000000000, 0.000000000000000000 ) ) ;
#71614=CARTESIAN_POINT ( 'NONE',  ( -16.87683809663752399, 51.08261412647723887, -232.2799364306433461 ) ) ;
#71712=AXIS2_PLACEMENT_3D ( 'NONE', #70544, #229594, #210040 ) ;
#71902=ADVANCED_FACE ( 'NONE', ( #103370 ), #182949, .F. ) ;
#71971=CARTESIAN_POINT ( 'NONE',  ( -14.00000000000000178, 47.91805600923872532, -233.7139610577891631 ) ) ;
#71985=ORIENTED_EDGE ( 'NONE', *, *, #137904, .T. ) ;
#72270=DIRECTION ( 'NONE',  ( 1.000000000000000000, 0.000000000000000000, 0.000000000000000000 ) ) ;
#72435=CARTESIAN_POINT ( 'NONE',  ( 14.11444803880196730, 46.48141361689233975, -234.7877205119061728 ) ) ;
#72483=ORIENTED_EDGE ( 'NONE', *, *, #232254, .T. ) ;
#72600=CARTESIAN_POINT ( 'NONE',  ( -16.93906926870270624, 44.02196362656498252, -235.2816881676999401 ) ) ;
#72730=DIRECTION ( 'NONE',  ( -1.000000000000000000, 0.000000000000000000, 0.000000000000000000 ) ) ;
#72834=DIRECTION ( 'NONE',  ( -0.000000000000000000, 0.9126074666063770380, 0.4088369013363281068 ) ) ;
#72974=( BOUNDED_SURFACE ( )  B_SPLINE_SURFACE ( 3, 2, ( 
 ( #143350, #181222, #179934 ),
 ( #220344, #203340, #243741 ),
 ( #219030, #121274, #241194 ),
 ( #139492, #84619, #159096 ) ),
 .UNSPECIFIED., .F., .F., .F. ) 
 B_SPLINE_SURFACE_WITH_KNOTS ( ( 4, 4 ),
 ( 3, 3 ),
 ( 0.0008258556059633821332, 0.0009616864997633045326 ),
 ( 0.000000000000000000, 1.000000000000000000 ),
 .UNSPECIFIED. ) 
 GEOMETRIC_REPRESENTATION_ITEM ( )  RATIONAL_B_SPLINE_SURFACE ( (
 ( 1.000000000000000000, 0.9152888060719758245, 1.000000000000000000),
 ( 1.000000000000000000, 0.9327727094137872044, 1.000000000000000000),
 ( 1.000000000000000000, 0.9369023509258540550, 1.000000000000000000),
 ( 1.000000000000000000, 0.9246339933864557992, 1.000000000000000000) ) ) 
 REPRESENTATION_ITEM ( '' )  SURFACE ( )  );
#73186=CARTESIAN_POINT ( 'NONE',  ( -18.40000000000000213, 40.40436687347765599, -235.2865959907995546 ) ) ;
#73254=ADVANCED_FACE ( 'NONE', ( #181410 ), #40636, .F. ) ;
#73335=EDGE_LOOP ( 'NONE', ( #46547, #240616, #13487, #212118 ) ) ;
#73656=CARTESIAN_POINT ( 'NONE',  ( -16.97683809663752186, 44.86297841676466902, -235.0825981793917094 ) ) ;
#73724=CARTESIAN_POINT ( 'NONE',  ( 13.54556439290364622, 46.53556350520270257, -234.7709563976631273 ) ) ;
#73837=CARTESIAN_POINT ( 'NONE',  ( -16.83558968593868244, 51.60763312609429221, -231.9514998304251492 ) ) ;
#73968=EDGE_LOOP ( 'NONE', ( #45665, #220118, #221230, #2582 ) ) ;
#74012=VERTEX_POINT ( 'NONE', #100856 ) ;
#74130=( GEOMETRIC_REPRESENTATION_CONTEXT ( 3 ) GLOBAL_UNCERTAINTY_ASSIGNED_CONTEXT ( ( #2310 ) ) GLOBAL_UNIT_ASSIGNED_CONTEXT ( ( #192241, #52698, #93114 ) ) REPRESENTATION_CONTEXT ( 'NONE', 'WORKASPACE' ) );
#74252=EDGE_CURVE ( 'NONE', #225390, #63280, #226830, .T. ) ;
#74300=AXIS2_PLACEMENT_3D ( 'NONE', #158118, #197188, #255836 ) ;
#74325=AXIS2_PLACEMENT_3D ( 'NONE', #210215, #169833, #249342 ) ;
#74532=PRODUCT ( 'Snap Open Cable Crossbars 9', 'Snap Open Cable Crossbars 9', '', ( #160344 ) ) ;
#74866=AXIS2_PLACEMENT_3D ( 'NONE', #138422, #194605, #173784 ) ;
#75024=VERTEX_POINT ( 'NONE', #32492 ) ;
#75038=CARTESIAN_POINT ( 'NONE',  ( -20.65000000000000568, 42.79061499530347845, -240.6131891775583824 ) ) ;
#75526=EDGE_LOOP ( 'NONE', ( #66702, #128592 ) ) ;
#75561=CYLINDRICAL_SURFACE ( 'NONE', #98504, 0.1000000000000090400 ) ;
#75831=ORIENTED_EDGE ( 'NONE', *, *, #105806, .T. ) ;
#76253=CARTESIAN_POINT ( 'NONE',  ( 14.77516762759922209, 46.65138127958493897, -234.7343221152024739 ) ) ;
#76589=CARTESIAN_POINT ( 'NONE',  ( -18.40000000000000213, 43.42149616655404287, -233.9497663708821165 ) ) ;
#76663=CARTESIAN_POINT ( 'NONE',  ( -13.54795643572458097, 46.53494637834451453, -234.7711487335851643 ) ) ;
#76664=CARTESIAN_POINT ( 'NONE',  ( 20.27550659511088682, 41.33268472976309482, -237.3587910501520071 ) ) ;
#76932=B_SPLINE_CURVE_WITH_KNOTS ( 'NONE', 3,
 ( #149865, #71614, #87283, #110719, #151144, #67743, #147275, #169453, #207273, #108158, #226809, #48169, #187710, #127726 ),
 .UNSPECIFIED., .F., .F.,
 ( 4, 2, 2, 2, 2, 2, 4 ),
 ( 6.938893903907227607E-18, 0.0003823333598417784991, 0.0005735000397626514044, 0.0006690833797230878299, 0.0007168750497033175894, 0.0007407708846934301381, 0.0007646667196835427952 ),
 .UNSPECIFIED. ) ;
#76940=PLANE ( 'NONE',  #12997 ) ;
#77021=CYLINDRICAL_SURFACE ( 'NONE', #152370, 1.749999999999999778 ) ;
#77046=VECTOR ( 'NONE', #164599, 1000.000000000000000 ) ;
#77176=EDGE_LOOP ( 'NONE', ( #5965, #67015, #137179, #48417 ) ) ;
#77528=DIRECTION ( 'NONE',  ( 0.000000000000000000, 0.6603344063872684799, -0.7509716850462297977 ) ) ;
#77626=CARTESIAN_POINT ( 'NONE',  ( -16.87998658237754412, 51.42389386751093383, -232.0338127545263944 ) ) ;
#77651=CARTESIAN_POINT ( 'NONE',  ( -16.97092634996615956, 51.61617950461997850, -231.8919089950969692 ) ) ;
#77776=ORIENTED_EDGE ( 'NONE', *, *, #197140, .F. ) ;
#77934=VERTEX_POINT ( 'NONE', #121621 ) ;
#77977=CARTESIAN_POINT ( 'NONE',  ( -15.31895204843005942, 49.15836891943285281, -233.6552066833103538 ) ) ;
#77978=CARTESIAN_POINT ( 'NONE',  ( -18.40000000000000213, 43.39957528361355799, -233.6562381667159798 ) ) ;
#78020=CIRCLE ( 'NONE', #44722, 0.09999999999999609201 ) ;
#78141=EDGE_CURVE ( 'NONE', #13111, #162125, #252760, .T. ) ;
#78168=CARTESIAN_POINT ( 'NONE',  ( -18.39418127959864790, 54.09461110551220742, -229.1565698459269811 ) ) ;
#78209=ORIENTED_EDGE ( 'NONE', *, *, #41553, .T. ) ;
#78554=VECTOR ( 'NONE', #50847, 1000.000000000000114 ) ;
#78578=CARTESIAN_POINT ( 'NONE',  ( -16.27683809663750480, 51.95542581965366935, -232.4531498054797680 ) ) ;
#78729=( NAMED_UNIT ( * ) PLANE_ANGLE_UNIT ( ) SI_UNIT ( $, .RADIAN. ) );
#78814=DIRECTION ( 'NONE',  ( 0.000000000000000000, -0.4088369013363281068, 0.9126074666063770380 ) ) ;
#78883=CARTESIAN_POINT ( 'NONE',  ( 13.54577453029515688, 49.62720671425051933, -233.3859273903070459 ) ) ;
#78916=CARTESIAN_POINT ( 'NONE',  ( -20.65000000000000568, 42.79061499530347845, -240.6131891775583824 ) ) ;
#79207=VERTEX_POINT ( 'NONE', #95777 ) ;
#79216=CARTESIAN_POINT ( 'NONE',  ( -12.29659703204452015, 47.69902910524212558, -234.3535107520373799 ) ) ;
#79229=CARTESIAN_POINT ( 'NONE',  ( 18.39999999999999503, 50.88295650978584206, -230.3037755757580953 ) ) ;
#79247=CARTESIAN_POINT ( 'NONE',  ( -15.06720934482788543, 49.36478519392533570, -233.5395520442457382 ) ) ;
#79253=VECTOR ( 'NONE', #5364, 1000.000000000000114 ) ;
#79377=DIRECTION ( 'NONE',  ( -0.7071067811865487940, -0.2890913453342118800, 0.6453109281988440582 ) ) ;
#79544=ORIENTED_EDGE ( 'NONE', *, *, #97066, .T. ) ;
#79552=AXIS2_PLACEMENT_3D ( 'NONE', #189549, #211686, #129567 ) ;
#79586=DIRECTION ( 'NONE',  ( 0.000000000000000000, 0.9126074666063771490, 0.4088369013363276627 ) ) ;
#79683=CARTESIAN_POINT ( 'NONE',  ( 18.39999999999999503, 43.51275691321468031, -233.9088826807484622 ) ) ;
#79701=VECTOR ( 'NONE', #9794, 1000.000000000000114 ) ;
#79747=CARTESIAN_POINT ( 'NONE',  ( 18.54999999999999716, 52.10946721379481517, -233.0415979755771900 ) ) ;
#79757=ORIENTED_EDGE ( 'NONE', *, *, #112376, .F. ) ;
#80007=CARTESIAN_POINT ( 'NONE',  ( 17.74533788810829904, 53.39598356028773907, -230.1986723552803653 ) ) ;
#80394=ORIENTED_EDGE ( 'NONE', *, *, #103688, .T. ) ;
#80521=CARTESIAN_POINT ( 'NONE',  ( -14.87770893841227426, 49.47508301341329684, -233.4759538034894319 ) ) ;
#80820=ORIENTED_EDGE ( 'NONE', *, *, #41553, .F. ) ;
#80982=DIRECTION ( 'NONE',  ( 0.8049926720990051576, -0.2425566999317299299, 0.5414360951997311266 ) ) ;
#81052=EDGE_CURVE ( 'NONE', #210192, #120740, #19744, .T. ) ;
#81057=CARTESIAN_POINT ( 'NONE',  ( -23.25000000000000355, 42.79061499530347845, -240.6131891775583824 ) ) ;
#81143=DIRECTION ( 'NONE',  ( 1.186688945009010077E-16, 0.4088369013363281623, -0.9126074666063771490 ) ) ;
#81282=CARTESIAN_POINT ( 'NONE',  ( 20.27550659511089037, 51.91893134239706598, -232.6162829946506179 ) ) ;
#81288=VECTOR ( 'NONE', #97247, 1000.000000000000000 ) ;
#81448=CARTESIAN_POINT ( 'NONE',  ( 12.25000000000000000, 48.12247445990688277, -234.1702647910923361 ) ) ;
#81756=ORIENTED_EDGE ( 'NONE', *, *, #38611, .T. ) ;
#81920=FACE_OUTER_BOUND ( 'NONE', #122011, .T. ) ;
#81967=DIRECTION ( 'NONE',  ( -0.000000000000000000, 0.9126074666063770380, 0.4088369013363281068 ) ) ;
#82105=DIRECTION ( 'NONE',  ( 0.5932847527679298016, 0.3291107096594074188, -0.7346423231209712190 ) ) ;
#82250=DIRECTION ( 'NONE',  ( -0.000000000000000000, 0.9126074666063769270, 0.4088369013363280513 ) ) ;
#82596=VECTOR ( 'NONE', #38140, 1000.000000000000227 ) ;
#82743=CARTESIAN_POINT ( 'NONE',  ( -16.89081410710458542, 51.62234474387415872, -231.9434644128527054 ) ) ;
#82839=ORIENTED_EDGE ( 'NONE', *, *, #182180, .F. ) ;
#82987=AXIS2_PLACEMENT_3D ( 'NONE', #46661, #104060, #242306 ) ;
#83396=VECTOR ( 'NONE', #126274, 1000.000000000000114 ) ;
#83480=ORIENTED_EDGE ( 'NONE', *, *, #220656, .F. ) ;
#83508=ORIENTED_EDGE ( 'NONE', *, *, #78141, .T. ) ;
#83601=CARTESIAN_POINT ( 'NONE',  ( 18.54999999999999716, 42.27269979661959098, -221.1123729563994402 ) ) ;
#83727=DIRECTION ( 'NONE',  ( -0.000000000000000000, 0.9126074666063769270, 0.4088369013363280513 ) ) ;
#83783=DIRECTION ( 'NONE',  ( -1.186688945009010077E-16, -0.4088369013363280513, 0.9126074666063769270 ) ) ;
#83789=EDGE_LOOP ( 'NONE', ( #28967, #128896, #9430, #231242, #107968, #35764 ) ) ;
#84160=CARTESIAN_POINT ( 'NONE',  ( -17.11825945287482753, 44.22674245267958781, -235.2580479164737994 ) ) ;
#84375=( BOUNDED_CURVE ( )  B_SPLINE_CURVE ( 3, ( #68892, #66310, #49305, #10197 ),
 .UNSPECIFIED., .F., .F. ) 
 B_SPLINE_CURVE_WITH_KNOTS ( ( 4, 4 ),
 ( 0.3000847527772395051, 0.5517402753107892854 ),
 .UNSPECIFIED. ) 
 CURVE ( )  GEOMETRIC_REPRESENTATION_ITEM ( )  RATIONAL_B_SPLINE_CURVE ( ( 1.000000000000000000, 0.9947294176030464508, 0.9947294176030464508, 1.000000000000000000 ) ) 
 REPRESENTATION_ITEM ( '' )  );
#84430=CARTESIAN_POINT ( 'NONE',  ( -16.94445028196808778, 44.07934375239701552, -235.2779890399608576 ) ) ;
#84520=CIRCLE ( 'NONE', #117867, 0.9000000000000014655 ) ;
#84619=CARTESIAN_POINT ( 'NONE',  ( -16.92570016628984320, 51.64205409960519688, -231.9264490580749225 ) ) ;
#84653=EDGE_CURVE ( 'NONE', #32681, #230513, #29691, .T. ) ;
#84662=CARTESIAN_POINT ( 'NONE',  ( -16.77828822459933633, 51.60887986673044026, -231.9550730111018026 ) ) ;
#84750=( BOUNDED_SURFACE ( )  B_SPLINE_SURFACE ( 3, 2, ( 
 ( #112936, #252422, #155938 ),
 ( #13836, #235428, #15124 ),
 ( #56771, #256217, #196309 ),
 ( #114214, #116780, #17666 ),
 ( #192471, #77626, #93359 ),
 ( #136312, #133770, #37267 ),
 ( #236711, #94642, #172950 ),
 ( #197593, #153387, #73837 ),
 ( #232906, #54228, #193754 ),
 ( #58067, #137605, #154656 ) ),
 .UNSPECIFIED., .F., .F., .T. ) 
 B_SPLINE_SURFACE_WITH_KNOTS ( ( 4, 2, 2, 2, 4 ),
 ( 3, 3 ),
 ( 0.002161241639767249104, 0.002579950749615824834, 0.002789305304540112482, 0.002893982582002256523, 0.002998659859464400564 ),
 ( 0.000000000000000000, 1.000000000000000000 ),
 .UNSPECIFIED. ) 
 GEOMETRIC_REPRESENTATION_ITEM ( )  RATIONAL_B_SPLINE_SURFACE ( (
 ( 1.000000000000000000, 0.7071067811865475727, 1.000000000000000000),
 ( 1.000000000000000000, 0.7632447400642182744, 1.000000000000000000),
 ( 1.000000000000000000, 0.8158073005138901657, 1.000000000000000000),
 ( 1.000000000000000000, 0.8906973462381438944, 1.000000000000000000),
 ( 1.000000000000000000, 0.9149408947793837843, 1.000000000000000000),
 ( 1.000000000000000000, 0.9493368785279248101, 1.000000000000000000),
 ( 1.000000000000000000, 0.9605194247155099951, 1.000000000000000000),
 ( 1.000000000000000000, 0.9803630264783056436, 1.000000000000000000),
 ( 1.000000000000000000, 0.9900844824269788846, 1.000000000000000000),
 ( 1.000000000000000000, 0.9894588281429261833, 1.000000000000000000) ) ) 
 REPRESENTATION_ITEM ( '' )  SURFACE ( )  );
#84914=ADVANCED_FACE ( 'NONE', ( #169800 ), #34137, .F. ) ;
#84957=CARTESIAN_POINT ( 'NONE',  ( -16.86132326855786090, 44.17986708625154790, -235.2790475031096378 ) ) ;
#85195=CARTESIAN_POINT ( 'NONE',  ( -18.40000000000000213, 45.89348038176515843, -239.2231437130149061 ) ) ;
#85230=MECHANICAL_DESIGN_GEOMETRIC_PRESENTATION_REPRESENTATION('',(#47647),#151933);
#85290=ORIENTED_EDGE ( 'NONE', *, *, #174157, .T. ) ;
#85565=LINE ( 'NONE', #46465, #64289 ) ;
#85584=AXIS2_PLACEMENT_3D ( 'NONE', #6528, #164342, #41842 ) ;
#85710=EDGE_CURVE ( 'NONE', #56126, #109657, #221542, .T. ) ;
#85725=CARTESIAN_POINT ( 'NONE',  ( -16.89268316805466341, 44.12952801035616801, -235.2997120924900969 ) ) ;
#85783=LINE ( 'NONE', #164083, #152419 ) ;
#86230=AXIS2_PLACEMENT_3D ( 'NONE', #4277, #64271, #83783 ) ;
#86351=EDGE_CURVE ( 'NONE', #251476, #212682, #37748, .T. ) ;
#86424=ORIENTED_EDGE ( 'NONE', *, *, #166041, .T. ) ;
#87044=ORIENTED_EDGE ( 'NONE', *, *, #213326, .F. ) ;
#87172=CARTESIAN_POINT ( 'NONE',  ( -16.86757978335471719, 44.08163191180170770, -235.3059065703284318 ) ) ;
#87283=CARTESIAN_POINT ( 'NONE',  ( -16.87372397896795562, 51.19159386254698774, -232.2139266409263598 ) ) ;
#87336=PLANE ( 'NONE',  #35698 ) ;
#87422=LINE ( 'NONE', #223085, #99387 ) ;
#87614=LINE ( 'NONE', #151488, #232497 ) ;
#87950=CIRCLE ( 'NONE', #58740, 0.1000000000000001721 ) ;
#87959=EDGE_LOOP ( 'NONE', ( #149498, #116075, #83480, #216670 ) ) ;
#88221=CARTESIAN_POINT ( 'NONE',  ( 18.54999999999999716, 41.52322060116084401, -237.7841060310786077 ) ) ;
#88269=CARTESIAN_POINT ( 'NONE',  ( -16.92280123533699054, 44.31858025389571054, -235.2169057130089129 ) ) ;
#88674=EDGE_CURVE ( 'NONE', #165639, #184724, #116374, .T. ) ;
#88786=ORIENTED_EDGE ( 'NONE', *, *, #234621, .F. ) ;
#88911=ORIENTED_EDGE ( 'NONE', *, *, #62588, .T. ) ;
#89172=CARTESIAN_POINT ( 'NONE',  ( -17.78241384948270110, 41.57411277420364826, -235.4540984113116906 ) ) ;
#89389=EDGE_CURVE ( 'NONE', #91807, #114829, #97448, .T. ) ;
#89572=CARTESIAN_POINT ( 'NONE',  ( -16.80891096016330977, 44.11936249622485917, -235.3061528139998586 ) ) ;
#89824=EDGE_CURVE ( 'NONE', #8358, #163693, #20560, .T. ) ;
#89825=CARTESIAN_POINT ( 'NONE',  ( -16.78270389226387138, 51.61191257970394020, -231.9524616731252138 ) ) ;
#89991=LINE ( 'NONE', #172154, #78554 ) ;
#90032=CARTESIAN_POINT ( 'NONE',  ( -21.64999999999999858, 44.38078384682074784, -235.8464960865713067 ) ) ;
#90106=CARTESIAN_POINT ( 'NONE',  ( 20.04999999999999716, 52.10946721379481517, -233.0415979755771900 ) ) ;
#90227=FACE_OUTER_BOUND ( 'NONE', #165381, .T. ) ;
#90474=CARTESIAN_POINT ( 'NONE',  ( -16.81744102076749314, 44.13548170601895038, -235.2989316066074821 ) ) ;
#90600=EDGE_LOOP ( 'NONE', ( #82839, #153594, #232746, #29902 ) ) ;
#90750=CARTESIAN_POINT ( 'NONE',  ( -16.92563707711778065, 51.63916908934552907, -231.9165628382792761 ) ) ;
#90816=CARTESIAN_POINT ( 'NONE',  ( -23.25000000000000355, 43.39957528361355799, -233.6562381667159798 ) ) ;
#90861=CARTESIAN_POINT ( 'NONE',  ( -16.83233564386408787, 44.25808114483436384, -235.2656807595939767 ) ) ;
#91028=EDGE_CURVE ( 'NONE', #240784, #162878, #190946, .T. ) ;
#91217=CARTESIAN_POINT ( 'NONE',  ( -17.11825945287481332, 51.52760218553060412, -231.9873527057832234 ) ) ;
#91298=LINE ( 'NONE', #169594, #91501 ) ;
#91389=CARTESIAN_POINT ( 'NONE',  ( -16.77683809663752257, 44.14991418685006153, -235.2970290647049580 ) ) ;
#91446=ADVANCED_FACE ( 'NONE', ( #172012 ), #250221, .F. ) ;
#91501=VECTOR ( 'NONE', #133000, 1000.000000000000000 ) ;
#91787=LINE ( 'NONE', #93060, #55865 ) ;
#91807=VERTEX_POINT ( 'NONE', #90816 ) ;
#92138=CARTESIAN_POINT ( 'NONE',  ( -16.93772744219066340, 44.07028146185461281, -235.2804298480971568 ) ) ;
#92372=CARTESIAN_POINT ( 'NONE',  ( -18.40000000000000213, 41.49355468354239207, -237.7178856438439141 ) ) ;
#92633=AXIS2_PLACEMENT_3D ( 'NONE', #21873, #101347, #2279 ) ;
#92634=CARTESIAN_POINT ( 'NONE',  ( -33.72168855820451938, 51.61886293219128419, -231.9464690156495124 ) ) ;
#92683=DIRECTION ( 'NONE',  ( 1.000000000000000000, 0.000000000000000000, 0.000000000000000000 ) ) ;
#93060=CARTESIAN_POINT ( 'NONE',  ( -16.87683809663752399, 44.17636539615257618, -235.3901923532681053 ) ) ;
#93114=( NAMED_UNIT ( * ) SI_UNIT ( $, .STERADIAN. ) SOLID_ANGLE_UNIT ( ) );
#93252=CARTESIAN_POINT ( 'NONE',  ( 12.25000000000000000, 48.12247445990688277, -234.1702647910923361 ) ) ;
#93309=CARTESIAN_POINT ( 'NONE',  ( 18.39999999999997371, 54.09900352584866567, -229.1663746252470446 ) ) ;
#93359=CARTESIAN_POINT ( 'NONE',  ( -16.92280123533709002, 51.43576438431487219, -232.0284949092479962 ) ) ;
#93413=CARTESIAN_POINT ( 'NONE',  ( -16.94107738177415712, 44.01795756907898749, -235.2811900454759666 ) ) ;
#93427=EDGE_CURVE ( 'NONE', #165639, #183570, #43843, .T. ) ;
#93528=ORIENTED_EDGE ( 'NONE', *, *, #30916, .F. ) ;
#93588=CARTESIAN_POINT ( 'NONE',  ( -18.40000000000000213, 40.40436687347765599, -235.2865959907995546 ) ) ;
#93673=ORIENTED_EDGE ( 'NONE', *, *, #236449, .F. ) ;
#93793=ORIENTED_EDGE ( 'NONE', *, *, #96264, .T. ) ;
#93892=CIRCLE ( 'NONE', #135574, 0.5000000000000004441 ) ;
#94110=EDGE_CURVE ( 'NONE', #14805, #48836, #21121, .T. ) ;
#94275=FACE_OUTER_BOUND ( 'NONE', #214397, .T. ) ;
#94351=VECTOR ( 'NONE', #165676, 1000.000000000000114 ) ;
#94530=CARTESIAN_POINT ( 'NONE',  ( 12.29592348164039528, 47.70130725485972789, -234.3525798712488495 ) ) ;
#94575=VECTOR ( 'NONE', #40937, 1000.000000000000114 ) ;
#94584=ORIENTED_EDGE ( 'NONE', *, *, #26694, .F. ) ;
#94642=CARTESIAN_POINT ( 'NONE',  ( -16.84793658983461029, 51.54252634946470835, -231.9806668642130774 ) ) ;
#94832=PLANE ( 'NONE',  #133634 ) ;
#94941=CARTESIAN_POINT ( 'NONE',  ( -15.75000000000000000, 47.91396133265956792, -234.2636761031307913 ) ) ;
#95017=CARTESIAN_POINT ( 'NONE',  ( -16.77902162784673834, 44.14788894467815084, -235.2972969561471075 ) ) ;
#95506=EDGE_CURVE ( 'NONE', #228856, #243788, #195643, .T. ) ;
#95542=CARTESIAN_POINT ( 'NONE',  ( -16.89021194854739605, 51.52081980694187990, -231.9903911278292981 ) ) ;
#95595=AXIS2_PLACEMENT_3D ( 'NONE', #200667, #203224, #22040 ) ;
#95619=DIRECTION ( 'NONE',  ( -1.652117596168391897E-15, 0.4088369013363280513, -0.9126074666063769270 ) ) ;
#95777=CARTESIAN_POINT ( 'NONE',  ( -16.87036670365548474, 51.72098459467785858, -231.8575261499355236 ) ) ;
#95804=CARTESIAN_POINT ( 'NONE',  ( 13.43443725621853879, 46.56801681390926007, -234.7608386620030387 ) ) ;
#96199=LINE ( 'NONE', #211035, #180980 ) ;
#96226=CARTESIAN_POINT ( 'NONE',  ( -14.56556274378147542, 46.56801681390926007, -234.7608386620030956 ) ) ;
#96264=EDGE_CURVE ( 'NONE', #251476, #237540, #13792, .T. ) ;
#96286=CARTESIAN_POINT ( 'NONE',  ( -16.77977881697926676, 44.14725513176800575, -235.2973807268633379 ) ) ;
#96565=DIRECTION ( 'NONE',  ( 0.000000000000000000, -0.9126074666063770380, -0.4088369013363281068 ) ) ;
#96956=ORIENTED_EDGE ( 'NONE', *, *, #155569, .T. ) ;
#97066=EDGE_CURVE ( 'NONE', #56126, #150070, #211180, .T. ) ;
#97247=DIRECTION ( 'NONE',  ( -1.000000000000000000, -9.792504721693619684E-16, -4.386921467590155985E-16 ) ) ;
#97448=LINE ( 'NONE', #256489, #214002 ) ;
#97557=CARTESIAN_POINT ( 'NONE',  ( -16.77683809663752257, 44.14991418685006153, -235.2970290647049580 ) ) ;
#97820=FACE_OUTER_BOUND ( 'NONE', #31750, .T. ) ;
#97867=CARTESIAN_POINT ( 'NONE',  ( -16.87036670365549895, 44.00112830765706917, -235.3159266546824995 ) ) ;
#98356=ORIENTED_EDGE ( 'NONE', *, *, #167062, .T. ) ;
#98473=CARTESIAN_POINT ( 'NONE',  ( -17.05016517656313724, 51.59814857156833057, -231.9557487940004705 ) ) ;
#98504=AXIS2_PLACEMENT_3D ( 'NONE', #117232, #172110, #132957 ) ;
#98532=B_SPLINE_CURVE_WITH_KNOTS ( 'NONE', 3,
 ( #85725, #23257, #46616, #204415, #161475, #7511, #2360, #123617, #121078, #84430 ),
 .UNSPECIFIED., .F., .F.,
 ( 4, 3, 3, 4 ),
 ( 1.894079734586027345E-15, 3.877043166999228241E-05, 7.336897548477449270E-05, 7.659383120240587149E-05 ),
 .UNSPECIFIED. ) ;
#98572=EDGE_CURVE ( 'NONE', #63280, #228856, #145441, .T. ) ;
#98759=CARTESIAN_POINT ( 'NONE',  ( -14.23072895065542731, 46.49260333018393965, -234.7842902611276656 ) ) ;
#98797=CARTESIAN_POINT ( 'NONE',  ( -13.11924609551135212, 49.48471825922439393, -233.4704840993163373 ) ) ;
#98832=CARTESIAN_POINT ( 'NONE',  ( -16.81095280782811230, 44.13548170601814746, -235.2989316066078231 ) ) ;
#99069=VECTOR ( 'NONE', #113455, 1000.000000000000114 ) ;
#99149=DIRECTION ( 'NONE',  ( 1.000000000000000000, 0.000000000000000000, 0.000000000000000000 ) ) ;
#99387=VECTOR ( 'NONE', #124009, 1000.000000000000000 ) ;
#99535=CARTESIAN_POINT ( 'NONE',  ( 15.48841904831874849, 44.70311864748992292, -236.5660131968816984 ) ) ;
#99582=B_SPLINE_CURVE_WITH_KNOTS ( 'NONE', 3,
 ( #138844, #178032, #257487, #217111, #39819, #157194, #201420, #240559, #200151, #180585, #197565, #20236, #236685, #159740, #58038, #78883, #61922, #38512, #219694, #22819, #119329, #161030, #237973, #59307, #1919, #158479, #198853, #137578, #99729, #81448 ),
 .UNSPECIFIED., .F., .F.,
 ( 4, 2, 2, 2, 2, 2, 2, 2, 2, 2, 2, 2, 2, 2, 4 ),
 ( 0.000000000000000000, 0.0003422764154113521547, 0.0006845528308227043094, 0.001026829246234056518, 0.001369105661645408619, 0.002053658492468067934, 0.002738211323290727466, 0.003080487738702053762, 0.003422764154113380492, 0.003765040569524707222, 0.004107316984936033519, 0.004449593400347360249, 0.004791869815758686979, 0.005134146231170013709, 0.005476422646581340439 ),
 .UNSPECIFIED. ) ;
#99729=CARTESIAN_POINT ( 'NONE',  ( 12.25000000000000000, 48.22675593180859011, -234.1235479764714853 ) ) ;
#99892=CARTESIAN_POINT ( 'NONE',  ( -16.87851181299898684, 44.13533318390521032, -235.2989511082154195 ) ) ;
#99986=ORIENTED_EDGE ( 'NONE', *, *, #146752, .T. ) ;
#100088=CARTESIAN_POINT ( 'NONE',  ( -13.54036565897075661, 49.63592998410995705, -233.3809899335355453 ) ) ;
#100286=ADVANCED_FACE ( 'NONE', ( #66667 ), #151355, .F. ) ;
#100409=CARTESIAN_POINT ( 'NONE',  ( -16.27683809663751191, 44.28952310016010330, -235.8873797767049325 ) ) ;
#100418=EDGE_LOOP ( 'NONE', ( #12252, #55820, #69394, #109200, #57552 ) ) ;
#100516=DIRECTION ( 'NONE',  ( -1.020425574104004394E-15, -0.9126074666063769270, -0.4088369013363280513 ) ) ;
#100856=CARTESIAN_POINT ( 'NONE',  ( -18.40000000000000213, 51.05395640845380711, -230.6854822754303314 ) ) ;
#101073=DIRECTION ( 'NONE',  ( -1.000000000000000000, 7.709882115452463178E-15, -3.083952846180985271E-14 ) ) ;
#101326=CARTESIAN_POINT ( 'NONE',  ( -21.65000000000000213, 52.72272256579932304, -234.4105091754867942 ) ) ;
#101347=DIRECTION ( 'NONE',  ( 0.7071067811865487940, -0.2890913453342118800, 0.6453109281988440582 ) ) ;
#101438=ORIENTED_EDGE ( 'NONE', *, *, #254699, .F. ) ;
#101721=FACE_OUTER_BOUND ( 'NONE', #8395, .T. ) ;
#101956=CARTESIAN_POINT ( 'NONE',  ( -16.90137573187933029, 44.26180248075819890, -235.2423414558488162 ) ) ;
#102071=CARTESIAN_POINT ( 'NONE',  ( 16.87683809663750267, 44.13548170601895038, -235.2989316066074821 ) ) ;
#102369=DIRECTION ( 'NONE',  ( 1.000000000000000000, 2.312964634635739111E-14, -6.167905692361970542E-14 ) ) ;
#103080=DIRECTION ( 'NONE',  ( 1.000000000000000000, 0.000000000000000000, 0.000000000000000000 ) ) ;
#103110=CARTESIAN_POINT ( 'NONE',  ( 21.72449340488910252, 40.89608266988597052, -236.3842060787925163 ) ) ;
#103370=FACE_OUTER_BOUND ( 'NONE', #174347, .T. ) ;
#103423=( LENGTH_UNIT ( ) NAMED_UNIT ( * ) SI_UNIT ( .MILLI., .METRE. ) );
#103688=EDGE_CURVE ( 'NONE', #210551, #131243, #202752, .T. ) ;
#103812=CARTESIAN_POINT ( 'NONE',  ( -16.77683809663752257, 42.27269979661959098, -221.1123729563994402 ) ) ;
#103985=CARTESIAN_POINT ( 'NONE',  ( -16.87683809663752754, 44.73333735360450447, -235.1232642955197605 ) ) ;
#104060=DIRECTION ( 'NONE',  ( 0.7071067811865463515, 0.2890913453342135453, -0.6453109281988460566 ) ) ;
#104115=CARTESIAN_POINT ( 'NONE',  ( -20.65000000000000568, 45.23934133962703186, -237.7629717664446787 ) ) ;
#104284=CARTESIAN_POINT ( 'NONE',  ( -18.40000000000000213, 53.98582189624752914, -228.9137301112145622 ) ) ;
#104355=EDGE_CURVE ( 'NONE', #184724, #63280, #196384, .T. ) ;
#104554=ORIENTED_EDGE ( 'NONE', *, *, #212162, .T. ) ;
#104951=ORIENTED_EDGE ( 'NONE', *, *, #208918, .F. ) ;
#104999=CARTESIAN_POINT ( 'NONE',  ( -15.75000000000000355, 47.91805600923872532, -233.7139610577891631 ) ) ;
#105158=ADVANCED_FACE ( 'NONE', ( #223046 ), #183927, .T. ) ;
#105553=CARTESIAN_POINT ( 'NONE',  ( -23.25000000000000355, 50.88295650978584206, -230.3037755757580953 ) ) ;
#105562=AXIS2_PLACEMENT_3D ( 'NONE', #219480, #142508, #61707 ) ;
#105806=EDGE_CURVE ( 'NONE', #2285, #14789, #56582, .T. ) ;
#106142=CARTESIAN_POINT ( 'NONE',  ( -23.25000000000000355, 42.79061499530347845, -240.6131891775583824 ) ) ;
#106153=CARTESIAN_POINT ( 'NONE',  ( -16.91256925476570316, 44.01351207619228489, -235.3144196755796145 ) ) ;
#106381=DIRECTION ( 'NONE',  ( 1.000000000000000000, -4.851622311275599093E-17, 1.082981191754466866E-16 ) ) ;
#106792=DIRECTION ( 'NONE',  ( 0.000000000000000000, -0.9126074666063769270, -0.4088369013363280513 ) ) ;
#107014=LINE ( 'NONE', #129169, #245700 ) ;
#107188=VERTEX_POINT ( 'NONE', #79747 ) ;
#107231=CARTESIAN_POINT ( 'NONE',  ( 20.27550659511089037, 44.43555011622476769, -235.9687455856084739 ) ) ;
#107254=ORIENTED_EDGE ( 'NONE', *, *, #81052, .T. ) ;
#107276=CARTESIAN_POINT ( 'NONE',  ( -18.34374000495060386, 40.40989152675300033, -235.2989281452919954 ) ) ;
#107421=ORIENTED_EDGE ( 'NONE', *, *, #240035, .T. ) ;
#107849=CARTESIAN_POINT ( 'NONE',  ( -16.94309007106719633, 44.07787287466445747, -235.2784698230337881 ) ) ;
#107858=CARTESIAN_POINT ( 'NONE',  ( -16.88783316861821859, 44.22880863429497111, -235.2571222925663790 ) ) ;
#107968=ORIENTED_EDGE ( 'NONE', *, *, #20272, .T. ) ;
#108079=VERTEX_POINT ( 'NONE', #108920 ) ;
#108158=CARTESIAN_POINT ( 'NONE',  ( -16.80469485234343807, 51.58553706477307799, -231.9699984979453689 ) ) ;
#108365=DIRECTION ( 'NONE',  ( 1.000000000000000000, 0.000000000000000000, 0.000000000000000000 ) ) ;
#108388=ORIENTED_EDGE ( 'NONE', *, *, #135039, .F. ) ;
#108447=CARTESIAN_POINT ( 'NONE',  ( -17.29158576265544056, 42.84089317668978936, -235.4244268507395645 ) ) ;
#108470=CARTESIAN_POINT ( 'NONE',  ( -18.40000000000000213, 51.02008725058737326, -230.6098793974720422 ) ) ;
#108614=LINE ( 'NONE', #9505, #16588 ) ;
#108744=FACE_OUTER_BOUND ( 'NONE', #56161, .T. ) ;
#108775=AXIS2_PLACEMENT_3D ( 'NONE', #180339, #219437, #42127 ) ;
#108920=CARTESIAN_POINT ( 'NONE',  ( 18.54999999999999716, 44.62608598762253109, -236.3940605665350745 ) ) ;
#109087=PLANE ( 'NONE',  #21861 ) ;
#109115=FACE_OUTER_BOUND ( 'NONE', #124988, .T. ) ;
#109118=AXIS2_PLACEMENT_3D ( 'NONE', #219827, #178168, #38635 ) ;
#109148=CARTESIAN_POINT ( 'NONE',  ( -16.83794237512075398, 44.28527064927406087, -235.2577326575541576 ) ) ;
#109200=ORIENTED_EDGE ( 'NONE', *, *, #226859, .F. ) ;
#109265=CARTESIAN_POINT ( 'NONE',  ( 20.99999999999999645, 51.70063031245850027, -232.1289905089708441 ) ) ;
#109301=CARTESIAN_POINT ( 'NONE',  ( -16.88495309932519817, 44.11948899812239233, -235.3010259908169814 ) ) ;
#109369=ORIENTED_EDGE ( 'NONE', *, *, #89389, .T. ) ;
#109657=VERTEX_POINT ( 'NONE', #189494 ) ;
#109672=DIRECTION ( 'NONE',  ( -1.073024830501117923E-15, -0.9126074666063771490, -0.4088369013363281623 ) ) ;
#109675=CIRCLE ( 'NONE', #172279, 1.749999999999998002 ) ;
#109687=ORIENTED_EDGE ( 'NONE', *, *, #163832, .T. ) ;
#109808=CIRCLE ( 'NONE', #163818, 1.749999999999999778 ) ;
#109903=( BOUNDED_CURVE ( )  B_SPLINE_CURVE ( 3, ( #11154, #127249, #28182, #167684 ),
 .UNSPECIFIED., .F., .T. ) 
 B_SPLINE_CURVE_WITH_KNOTS ( ( 4, 4 ),
 ( 1.570796326794908992, 2.617993877991514395 ),
 .UNSPECIFIED. ) 
 CURVE ( )  GEOMETRIC_REPRESENTATION_ITEM ( )  RATIONAL_B_SPLINE_CURVE ( ( 1.000000000000000000, 0.9106836025229576581, 0.9106836025229576581, 1.000000000000000000 ) ) 
 REPRESENTATION_ITEM ( '' )  );
#109984=EDGE_CURVE ( 'NONE', #13111, #64755, #48375, .T. ) ;
#110097=CIRCLE ( 'NONE', #255806, 0.1000000000000024342 ) ;
#110311=CARTESIAN_POINT ( 'NONE',  ( 23.04999999999999716, 41.49355468354239207, -237.7178856438439141 ) ) ;
#110524=EDGE_LOOP ( 'NONE', ( #244124, #215610 ) ) ;
#110710=DIRECTION ( 'NONE',  ( 0.000000000000000000, 0.4088369013363281068, -0.9126074666063770380 ) ) ;
#110719=CARTESIAN_POINT ( 'NONE',  ( -16.85939681242906474, 51.35418898951247968, -232.1141021923019707 ) ) ;
#111011=CARTESIAN_POINT ( 'NONE',  ( -17.78043020864320667, 41.65515396761067279, -235.4199665519760458 ) ) ;
#111072=ORIENTED_EDGE ( 'NONE', *, *, #1185, .F. ) ;
#111088=CARTESIAN_POINT ( 'NONE',  ( 23.24999999999999645, 52.07980129617636322, -232.9753775883424964 ) ) ;
#111266=CARTESIAN_POINT ( 'NONE',  ( -16.81744102076748959, 51.61886293219124155, -231.9464690156495692 ) ) ;
#111341=ORIENTED_EDGE ( 'NONE', *, *, #123918, .F. ) ;
#111536=CLOSED_SHELL ( 'NONE', ( #100286, #14906, #129888, #181256, #84914, #135319, #56711, #183070, #137682, #234681, #166949, #204848, #128016, #196548, #33204, #42802, #158369, #52037, #133613, #31016, #192852, #218237, #61406, #91446, #73254, #50395, #161515, #21760, #54273, #193356, #42976, #184845, #114744, #224182, #26983, #117011, #248405, #71902, #135763, #10985, #14642, #251438, #148738, #191594, #5932, #243493, #134155, #105158, #167507, #30219, #250415, #236431, #30894 ) ) ;
#111574=CARTESIAN_POINT ( 'NONE',  ( -16.89268316805465986, 51.62340874627276577, -231.9425458505251072 ) ) ;
#111629=EDGE_LOOP ( 'NONE', ( #63675, #238649, #125710, #212758 ) ) ;
#111666=DIRECTION ( 'NONE',  ( 0.000000000000000000, 0.9126074666063769270, 0.4088369013363280513 ) ) ;
#111907=CARTESIAN_POINT ( 'NONE',  ( -16.86422026484316916, 44.06525935397618099, -235.3079849271810531 ) ) ;
#111955=EDGE_CURVE ( 'NONE', #131621, #91807, #108614, .T. ) ;
#112015=CARTESIAN_POINT ( 'NONE',  ( -23.25000000000000355, 40.29670989715187090, -235.0462836312595130 ) ) ;
#112074=AXIS2_PLACEMENT_3D ( 'NONE', #29757, #32318, #72730 ) ;
#112076=CARTESIAN_POINT ( 'NONE',  ( 23.24999999999999645, 44.59642007000408626, -236.3278401793003809 ) ) ;
#112083=EDGE_CURVE ( 'NONE', #2625, #126778, #162327, .T. ) ;
#112129=CARTESIAN_POINT ( 'NONE',  ( -16.93860193097147970, 51.64699553454050829, -231.8866301305883439 ) ) ;
#112217=CARTESIAN_POINT ( 'NONE',  ( -16.94445028196808778, 44.07934375239701552, -235.2779890399608576 ) ) ;
#112376=EDGE_CURVE ( 'NONE', #168251, #226785, #107014, .T. ) ;
#112385=ORIENTED_EDGE ( 'NONE', *, *, #124755, .F. ) ;
#112501=CARTESIAN_POINT ( 'NONE',  ( -16.94107738177415712, 44.01795756907898749, -235.2811900454759666 ) ) ;
#112573=( BOUNDED_SURFACE ( )  B_SPLINE_SURFACE ( 3, 2, ( 
 ( #39861, #155958, #235451 ),
 ( #136332, #37288, #77651 ),
 ( #157245, #98473, #20286 ),
 ( #178082, #119381, #198904 ) ),
 .UNSPECIFIED., .F., .F., .F. ) 
 B_SPLINE_SURFACE_WITH_KNOTS ( ( 4, 4 ),
 ( 3, 3 ),
 ( 3.658908243880891309, 4.712388980384689674 ),
 ( 0.000000000000000000, 1.000000000000000000 ),
 .UNSPECIFIED. ) 
 GEOMETRIC_REPRESENTATION_ITEM ( )  RATIONAL_B_SPLINE_SURFACE ( (
 ( 1.000000000000000000, 0.8984936768950106956, 1.000000000000000000),
 ( 1.000000000000000000, 0.8646876308618098861, 1.000000000000000000),
 ( 1.000000000000000000, 0.7953136715911073296, 1.000000000000000000),
 ( 1.000000000000000000, 0.7071067811866069697, 1.000000000000000000) ) ) 
 REPRESENTATION_ITEM ( '' )  SURFACE ( )  );
#112706=ORIENTED_EDGE ( 'NONE', *, *, #46537, .F. ) ;
#112800=DIRECTION ( 'NONE',  ( 0.000000000000000000, 0.9126074666063769270, 0.4088369013363280513 ) ) ;
#112936=CARTESIAN_POINT ( 'NONE',  ( -16.87683809663752399, 50.97313360171293084, -232.3453239361865315 ) ) ;
#112995=CARTESIAN_POINT ( 'NONE',  ( -16.93658211146646408, 44.06789837094380857, -235.2808755401713938 ) ) ;
#113241=EDGE_CURVE ( 'NONE', #172022, #75024, #121098, .T. ) ;
#113426=ORIENTED_EDGE ( 'NONE', *, *, #152813, .T. ) ;
#113455=DIRECTION ( 'NONE',  ( -1.652117596168391897E-15, 0.4088369013363281068, -0.9126074666063770380 ) ) ;
#113676=AXIS2_PLACEMENT_3D ( 'NONE', #30721, #33298, #112800 ) ;
#114023=CARTESIAN_POINT ( 'NONE',  ( -16.87331047859651179, 44.13548170601895038, -235.2989316066074821 ) ) ;
#114214=CARTESIAN_POINT ( 'NONE',  ( -16.85697194749120698, 51.37571476901084822, -232.1008225933170479 ) ) ;
#114482=DIRECTION ( 'NONE',  ( -1.000000000000000000, -0.000000000000000000, 0.000000000000000000 ) ) ;
#114592=CARTESIAN_POINT ( 'NONE',  ( -16.81744102076749314, 44.13548170601895038, -235.2989316066074821 ) ) ;
#114594=ORIENTED_EDGE ( 'NONE', *, *, #216011, .T. ) ;
#114674=CARTESIAN_POINT ( 'NONE',  ( -16.93234230245721861, 51.66096952035064049, -231.8748915850824801 ) ) ;
#114744=ADVANCED_FACE ( 'NONE', ( #198266, #138277, #217813 ), #256912, .T. ) ;
#114829=VERTEX_POINT ( 'NONE', #105553 ) ;
#114872=CARTESIAN_POINT ( 'NONE',  ( 20.27550659511089037, 51.91893134239705887, -232.6162829946506179 ) ) ;
#115273=ORIENTED_EDGE ( 'NONE', *, *, #42579, .F. ) ;
#115352=VERTEX_POINT ( 'NONE', #224586 ) ;
#115442=DIRECTION ( 'NONE',  ( -0.000000000000000000, 0.9126074666063769270, 0.4088369013363280513 ) ) ;
#115755=VECTOR ( 'NONE', #55400, 1000.000000000000114 ) ;
#115773=VECTOR ( 'NONE', #182994, 1000.000000000000114 ) ;
#115836=LINE ( 'NONE', #77978, #130491 ) ;
#116045=CARTESIAN_POINT ( 'NONE',  ( -18.38817693311004575, 54.09559807286957067, -229.1587729586515820 ) ) ;
#116075=ORIENTED_EDGE ( 'NONE', *, *, #215503, .T. ) ;
#116095=CARTESIAN_POINT ( 'NONE',  ( -18.40000000000000213, 43.57057518228153015, -234.0379448663882442 ) ) ;
#116096=VECTOR ( 'NONE', #203881, 1000.000000000000114 ) ;
#116120=CARTESIAN_POINT ( 'NONE',  ( -23.25000000000000355, 45.89348038176515843, -239.2231437130149061 ) ) ;
#116150=CARTESIAN_POINT ( 'NONE',  ( -16.97683809663752186, 44.17636539615257618, -235.3901923532681053 ) ) ;
#116158=DIRECTION ( 'NONE',  ( -0.000000000000000000, 0.9126074666063770380, 0.4088369013363281068 ) ) ;
#116205=CARTESIAN_POINT ( 'NONE',  ( -16.85718274719362597, 44.04571297885565428, -235.3105011521292909 ) ) ;
#116374=LINE ( 'NONE', #17275, #152809 ) ;
#116415=AXIS2_PLACEMENT_3D ( 'NONE', #71971, #31585, #12010 ) ;
#116780=CARTESIAN_POINT ( 'NONE',  ( -16.88705144915407175, 51.36243976870036931, -232.0613434336529508 ) ) ;
#116947=ORIENTED_EDGE ( 'NONE', *, *, #166041, .F. ) ;
#117011=ADVANCED_FACE ( 'NONE', ( #221735 ), #241343, .T. ) ;
#117091=CARTESIAN_POINT ( 'NONE',  ( -14.45443560709636444, 46.53556350520271678, -234.7709563976631841 ) ) ;
#117124=CARTESIAN_POINT ( 'NONE',  ( -14.22969084473441370, 49.66582466164803833, -233.3627041835000000 ) ) ;
#117210=EDGE_LOOP ( 'NONE', ( #64853, #224743 ) ) ;
#117232=CARTESIAN_POINT ( 'NONE',  ( -15.55912972643740488, 52.30666975485627290, -233.2371980086100507 ) ) ;
#117265=VECTOR ( 'NONE', #6412, 1000.000000000000000 ) ;
#117547=CARTESIAN_POINT ( 'NONE',  ( 18.39999999999999503, 45.89348038176515843, -239.2231437130149061 ) ) ;
#117802=ORIENTED_EDGE ( 'NONE', *, *, #150906, .T. ) ;
#117862=LINE ( 'NONE', #81282, #94575 ) ;
#117867=AXIS2_PLACEMENT_3D ( 'NONE', #145383, #141532, #101073 ) ;
#118257=DIRECTION ( 'NONE',  ( -1.646408749285562691E-14, -0.4088369013363281068, 0.9126074666063770380 ) ) ;
#118320=VECTOR ( 'NONE', #228970, 1000.000000000000114 ) ;
#118385=LINE ( 'NONE', #42685, #70338 ) ;
#118466=AXIS2_PLACEMENT_3D ( 'NONE', #116150, #37907, #120019 ) ;
#118746=CARTESIAN_POINT ( 'NONE',  ( 21.72449340488910607, 40.89608266988597052, -236.3842060787924879 ) ) ;
#118781=( BOUNDED_SURFACE ( )  B_SPLINE_SURFACE ( 3, 2, ( 
 ( #6167, #167852, #188666 ),
 ( #145679, #8754, #10031 ),
 ( #225204, #169144, #248642 ),
 ( #46573, #70032, #205650 ) ),
 .UNSPECIFIED., .F., .F., .T. ) 
 B_SPLINE_SURFACE_WITH_KNOTS ( ( 4, 4 ),
 ( 3, 3 ),
 ( 0.3000847527772392831, 0.5552748953338751958 ),
 ( 0.000000000000000000, 1.000000000000000000 ),
 .UNSPECIFIED. ) 
 GEOMETRIC_REPRESENTATION_ITEM ( )  RATIONAL_B_SPLINE_SURFACE ( (
 ( 1.000000000000000000, 0.9152888060719472918, 1.000000000000000000),
 ( 1.000000000000000000, 0.9104333467450296258, 1.000000000000000000),
 ( 1.000000000000000000, 0.9035312726220154911, 1.000000000000000000),
 ( 1.000000000000000000, 0.8946697475932554600, 1.000000000000000000) ) ) 
 REPRESENTATION_ITEM ( '' )  SURFACE ( )  );
#118868=ORIENTED_EDGE ( 'NONE', *, *, #153782, .F. ) ;
#119054=DIRECTION ( 'NONE',  ( -1.000000000000000000, -6.754466386607085130E-16, 1.507734853975053794E-15 ) ) ;
#119329=CARTESIAN_POINT ( 'NONE',  ( 12.84435279558019971, 49.30157392506335867, -233.5755204583867055 ) ) ;
#119381=CARTESIAN_POINT ( 'NONE',  ( -17.11825945287482043, 51.61886293219122024, -231.9464690156495976 ) ) ;
#119632=CARTESIAN_POINT ( 'NONE',  ( -23.25000000000000355, 51.48671849539696410, -231.8960919591225718 ) ) ;
#119699=CARTESIAN_POINT ( 'NONE',  ( -15.39126916658604216, 49.08063300121916939, -233.6976605013540222 ) ) ;
#120019=DIRECTION ( 'NONE',  ( -1.000000000000000000, 0.000000000000000000, 0.000000000000000000 ) ) ;
#120180=ORIENTED_EDGE ( 'NONE', *, *, #240113, .T. ) ;
#120244=( BOUNDED_SURFACE ( )  B_SPLINE_SURFACE ( 3, 2, ( 
 ( #84160, #163767, #226268 ),
 ( #42518, #47636, #141622 ),
 ( #243278, #221148, #144173 ),
 ( #201593, #131045, #31978 ) ),
 .UNSPECIFIED., .F., .F., .F. ) 
 B_SPLINE_SURFACE_WITH_KNOTS ( ( 4, 4 ),
 ( 3, 3 ),
 ( 4.712388980384689674, 5.765869716888459173 ),
 ( 0.000000000000000000, 1.000000000000000000 ),
 .UNSPECIFIED. ) 
 GEOMETRIC_REPRESENTATION_ITEM ( )  RATIONAL_B_SPLINE_SURFACE ( (
 ( 1.000000000000000000, 0.7071067811865497932, 1.000000000000000000),
 ( 1.000000000000000000, 0.7953136715912831889, 1.000000000000000000),
 ( 1.000000000000000000, 0.8646876308615263351, 1.000000000000000000),
 ( 1.000000000000000000, 0.8984936768950678720, 1.000000000000000000) ) ) 
 REPRESENTATION_ITEM ( '' )  SURFACE ( )  );
#120418=CARTESIAN_POINT ( 'NONE',  ( 17.23472005113827876, 42.89716137982957633, -235.4615306384476128 ) ) ;
#120698=CARTESIAN_POINT ( 'NONE',  ( 18.54999999999999716, 41.52322060116084401, -237.7841060310786077 ) ) ;
#120740=VERTEX_POINT ( 'NONE', #76589 ) ;
#121072=LINE ( 'NONE', #160192, #195405 ) ;
#121078=CARTESIAN_POINT ( 'NONE',  ( -16.94389599338512298, 44.07998477742863486, -235.2786503815312074 ) ) ;
#121098=B_SPLINE_CURVE_WITH_KNOTS ( 'NONE', 3,
 ( #93252, #194949, #94530, #232792, #16314, #253600, #154554, #252317, #211938, #95804, #73724, #254839, #150672, #72435, #230201, #136201, #54122, #76253, #52837, #171549, #33330, #251032, #133670, #155825, #235330, #215757 ),
 .UNSPECIFIED., .F., .F.,
 ( 4, 2, 2, 2, 2, 2, 2, 2, 2, 2, 2, 2, 4 ),
 ( 0.005476422646581340439, 0.006160811967703548782, 0.006845201288825757124, 0.007187395949386861729, 0.007529590609947966334, 0.007871785270509069204, 0.008213979931070173809, 0.008556174591631278414, 0.008898369252192381285, 0.009240563912753487624, 0.009582758573314590494, 0.01026714789443680491, 0.01095153721555902106 ),
 .UNSPECIFIED. ) ;
#121274=CARTESIAN_POINT ( 'NONE',  ( -16.90202395485708919, 51.66072493185733805, -231.9102439397140358 ) ) ;
#121325=DIRECTION ( 'NONE',  ( 0.7071067811865462405, 0.2890913453342134898, -0.6453109281988460566 ) ) ;
#121351=CARTESIAN_POINT ( 'NONE',  ( -16.87331047859651179, 44.13548170601895038, -235.2989316066074821 ) ) ;
#121532=VECTOR ( 'NONE', #252655, 1000.000000000000114 ) ;
#121605=CARTESIAN_POINT ( 'NONE',  ( -14.00000000000000178, 47.91805600923872532, -233.7139610577891631 ) ) ;
#121621=CARTESIAN_POINT ( 'NONE',  ( -21.64999999999999858, 44.09459801588531036, -235.2076708599468020 ) ) ;
#121751=FILL_AREA_STYLE_COLOUR ( '', #255908 ) ;
#121867=AXIS2_PLACEMENT_3D ( 'NONE', #103812, #106381, #43871 ) ;
#121923=CARTESIAN_POINT ( 'NONE',  ( -16.89208623190940273, 51.62302926044408480, -231.9428734964056389 ) ) ;
#122011=EDGE_LOOP ( 'NONE', ( #213181, #64584, #116947 ) ) ;
#122257=CARTESIAN_POINT ( 'NONE',  ( -12.42749937872396693, 48.82262352862033339, -233.8339354177745975 ) ) ;
#122794=LINE ( 'NONE', #81057, #79253 ) ;
#122873=EDGE_CURVE ( 'NONE', #243788, #131621, #115836, .T. ) ;
#123024=( LENGTH_UNIT ( ) NAMED_UNIT ( * ) SI_UNIT ( .MILLI., .METRE. ) );
#123260=CARTESIAN_POINT ( 'NONE',  ( -16.87036670365549895, 44.00112830765706917, -235.3159266546824995 ) ) ;
#123582=CARTESIAN_POINT ( 'NONE',  ( -16.87683809663749557, 44.82209472663102900, -234.9913374327310862 ) ) ;
#123617=CARTESIAN_POINT ( 'NONE',  ( -16.94333152886236959, 44.08063011399070774, -235.2792992266545298 ) ) ;
#123710=LINE ( 'NONE', #24632, #137494 ) ;
#123918=EDGE_CURVE ( 'NONE', #126778, #134853, #235815, .T. ) ;
#124009=DIRECTION ( 'NONE',  ( -1.000000000000000000, 5.751876041739926423E-15, -1.546394132359972529E-14 ) ) ;
#124208=CARTESIAN_POINT ( 'NONE',  ( -21.65000000000000213, 51.57797924205760864, -231.8552082689889460 ) ) ;
#124234=VECTOR ( 'NONE', #146165, 1000.000000000000114 ) ;
#124755=EDGE_CURVE ( 'NONE', #244889, #150070, #143873, .T. ) ;
#124757=VECTOR ( 'NONE', #212010, 1000.000000000000114 ) ;
#124988=EDGE_LOOP ( 'NONE', ( #237045, #196193, #240011, #93673, #70894 ) ) ;
#125126=CARTESIAN_POINT ( 'NONE',  ( 22.88900146558018989, 44.64493140999041998, -236.4361273983403180 ) ) ;
#125259=ORIENTED_EDGE ( 'NONE', *, *, #208252, .T. ) ;
#125416=CARTESIAN_POINT ( 'NONE',  ( -16.84421487269769102, 44.15327948857689933, -235.2909584192975672 ) ) ;
#125618=AXIS2_PLACEMENT_3D ( 'NONE', #201143, #119054, #95619 ) ;
#125710=ORIENTED_EDGE ( 'NONE', *, *, #163832, .F. ) ;
#125918=VERTEX_POINT ( 'NONE', #54170 ) ;
#126030=CARTESIAN_POINT ( 'NONE',  ( -16.94333152882356686, 51.64072791834932019, -231.8924685538414394 ) ) ;
#126127=CARTESIAN_POINT ( 'NONE',  ( -16.88705144915408596, 44.39190486951041237, -235.1840571886030489 ) ) ;
#126144=CARTESIAN_POINT ( 'NONE',  ( -16.87683809663752399, 44.86297841676450560, -235.0825981793917947 ) ) ;
#126269=VERTEX_POINT ( 'NONE', #134680 ) ;
#126274=DIRECTION ( 'NONE',  ( 0.000000000000000000, -0.4088369013363281068, 0.9126074666063770380 ) ) ;
#126279=CARTESIAN_POINT ( 'NONE',  ( -16.97683809663752186, 41.03261631955726330, -236.6889770711509584 ) ) ;
#126368=CARTESIAN_POINT ( 'NONE',  ( 16.27683809663750125, 41.27791846035906076, -237.2365415511148115 ) ) ;
#126720=AXIS2_PLACEMENT_3D ( 'NONE', #36912, #216783, #154305 ) ;
#126762=ORIENTED_EDGE ( 'NONE', *, *, #198016, .T. ) ;
#126778=VERTEX_POINT ( 'NONE', #145932 ) ;
#126980=ORIENTED_EDGE ( 'NONE', *, *, #243538, .F. ) ;
#127012=PLANE ( 'NONE',  #180383 ) ;
#127038=CARTESIAN_POINT ( 'NONE',  ( -16.87036670365549895, 43.98904843454555902, -235.2166589526560472 ) ) ;
#127241=CIRCLE ( 'NONE', #60581, 0.09999999999999939493 ) ;
#127249=CARTESIAN_POINT ( 'NONE',  ( -17.01473183483380325, 51.52760218553058280, -231.9873527057832234 ) ) ;
#127281=CARTESIAN_POINT ( 'NONE',  ( -16.86379686415369150, 51.68465521706279731, -231.8893622364056171 ) ) ;
#127543=DIRECTION ( 'NONE',  ( -1.073024830501117725E-15, 0.9126074666063770380, 0.4088369013363281068 ) ) ;
#127726=CARTESIAN_POINT ( 'NONE',  ( -16.77683809663752257, 51.60783545504968117, -231.9559722212415522 ) ) ;
#127790=ORIENTED_EDGE ( 'NONE', *, *, #232254, .F. ) ;
#127908=ORIENTED_EDGE ( 'NONE', *, *, #122873, .F. ) ;
#128016=ADVANCED_FACE ( 'NONE', ( #31222 ), #195412, .F. ) ;
#128064=ORIENTED_EDGE ( 'NONE', *, *, #89389, .F. ) ;
#128489=EDGE_CURVE ( 'NONE', #156660, #68788, #68269, .T. ) ;
#128592=ORIENTED_EDGE ( 'NONE', *, *, #135379, .T. ) ;
#128896=ORIENTED_EDGE ( 'NONE', *, *, #137989, .T. ) ;
#129101=DIRECTION ( 'NONE',  ( -0.000000000000000000, 0.9126074666063770380, 0.4088369013363281068 ) ) ;
#129112=ORIENTED_EDGE ( 'NONE', *, *, #111955, .F. ) ;
#129169=CARTESIAN_POINT ( 'NONE',  ( -20.65000000000000568, 45.23934133962703186, -237.7629717664446787 ) ) ;
#129180=EDGE_CURVE ( 'NONE', #57171, #7237, #121072, .T. ) ;
#129227=DIRECTION ( 'NONE',  ( -1.000000000000000000, -6.754466386607082172E-16, 1.507734853975053202E-15 ) ) ;
#129317=CARTESIAN_POINT ( 'NONE',  ( -18.40000000000000213, 51.05395640845380711, -230.6854822754303314 ) ) ;
#129341=DIRECTION ( 'NONE',  ( 1.000000000000000000, 0.000000000000000000, 0.000000000000000000 ) ) ;
#129567=DIRECTION ( 'NONE',  ( 1.000000000000000000, 0.000000000000000000, 0.000000000000000000 ) ) ;
#129682=ORIENTED_EDGE ( 'NONE', *, *, #180891, .F. ) ;
#129888=ADVANCED_FACE ( 'NONE', ( #16213 ), #250925, .F. ) ;
#129963=CARTESIAN_POINT ( 'NONE',  ( -16.94062896051973865, 44.07468280125904414, -235.2793588221107086 ) ) ;
#130491=VECTOR ( 'NONE', #33780, 1000.000000000000114 ) ;
#130729=EDGE_CURVE ( 'NONE', #156660, #162125, #16884, .T. ) ;
#130868=ORIENTED_EDGE ( 'NONE', *, *, #21175, .F. ) ;
#130869=VECTOR ( 'NONE', #8850, 1000.000000000000114 ) ;
#130871=CARTESIAN_POINT ( 'NONE',  ( -18.37013991200266005, 40.35975918565798537, -235.2922552195464618 ) ) ;
#131045=CARTESIAN_POINT ( 'NONE',  ( -16.91049119928364775, 44.10653343834928819, -235.3119000738687134 ) ) ;
#131052=CARTESIAN_POINT ( 'NONE',  ( -17.11825945287481332, 51.48671849539696410, -231.8960919591225718 ) ) ;
#131243=VERTEX_POINT ( 'NONE', #70793 ) ;
#131621=VERTEX_POINT ( 'NONE', #1488 ) ;
#131791=CARTESIAN_POINT ( 'NONE',  ( -18.40000000000000213, 43.53670602441511051, -233.9623419884299551 ) ) ;
#132070=EDGE_CURVE ( 'NONE', #79207, #172948, #84375, .T. ) ;
#132351=FACE_OUTER_BOUND ( 'NONE', #193173, .T. ) ;
#132526=CARTESIAN_POINT ( 'NONE',  ( -21.64999999999999858, 51.86416507299303902, -232.4940334956133938 ) ) ;
#132571=CARTESIAN_POINT ( 'NONE',  ( -16.82542659449996592, 44.22818387756893088, -235.2743865959531036 ) ) ;
#132905=EDGE_CURVE ( 'NONE', #204898, #131243, #156594, .T. ) ;
#132957=DIRECTION ( 'NONE',  ( -0.7071067811865019426, 0.2890913453341708572, -0.6453109281989138912 ) ) ;
#132970=CARTESIAN_POINT ( 'NONE',  ( -16.94445028196807002, 51.64060657411747712, -231.8906364537310196 ) ) ;
#133000=DIRECTION ( 'NONE',  ( -1.000000000000000000, -0.000000000000000000, 0.000000000000000000 ) ) ;
#133421=CIRCLE ( 'NONE', #58570, 0.1000000000000024342 ) ;
#133500=ORIENTED_EDGE ( 'NONE', *, *, #236081, .F. ) ;
#133533=SURFACE_STYLE_USAGE ( .BOTH. , #33195 ) ;
#133613=ADVANCED_FACE ( 'NONE', ( #150794 ), #109087, .F. ) ;
#133634=AXIS2_PLACEMENT_3D ( 'NONE', #195253, #118257, #159973 ) ;
#133635=CIRCLE ( 'NONE', #21251, 0.9000000000000014655 ) ;
#133670=CARTESIAN_POINT ( 'NONE',  ( 15.52844286134407881, 47.30686838571505604, -234.5075185885025633 ) ) ;
#133757=UNCERTAINTY_MEASURE_WITH_UNIT (LENGTH_MEASURE( 1.000000000000000082E-05 ), #103423, 'distance_accuracy_value', 'NONE');
#133770=CARTESIAN_POINT ( 'NONE',  ( -16.85722902420148372, 51.51341344488079699, -231.9937090867831273 ) ) ;
#134066=CARTESIAN_POINT ( 'NONE',  ( -15.15766958671843412, 46.89553527312529724, -234.6535825622729874 ) ) ;
#134128=ORIENTED_EDGE ( 'NONE', *, *, #170498, .F. ) ;
#134155=ADVANCED_FACE ( 'NONE', ( #101721 ), #12871, .T. ) ;
#134340=DIRECTION ( 'NONE',  ( -1.000000000000000000, 0.000000000000000000, 0.000000000000000000 ) ) ;
#134396=CARTESIAN_POINT ( 'NONE',  ( 20.73486653747088582, 42.13647595316533057, -239.1530172309881550 ) ) ;
#134417=LINE ( 'NONE', #229700, #209825 ) ;
#134680=CARTESIAN_POINT ( 'NONE',  ( 23.24999999999999645, 50.88295650978584206, -230.3037755757580953 ) ) ;
#134853=VERTEX_POINT ( 'NONE', #13902 ) ;
#135039=EDGE_CURVE ( 'NONE', #32277, #12028, #84520, .T. ) ;
#135076=ORIENTED_EDGE ( 'NONE', *, *, #84653, .F. ) ;
#135160=DIRECTION ( 'NONE',  ( 0.000000000000000000, 0.000000000000000000, 1.000000000000000000 ) ) ;
#135319=ADVANCED_FACE ( 'NONE', ( #240356 ), #181664, .F. ) ;
#135347=CARTESIAN_POINT ( 'NONE',  ( -15.06774609480954474, 46.82518482938919391, -234.6773041598980853 ) ) ;
#135379=EDGE_CURVE ( 'NONE', #246882, #152864, #109675, .T. ) ;
#135415=EDGE_CURVE ( 'NONE', #126778, #143787, #1715, .T. ) ;
#135574=AXIS2_PLACEMENT_3D ( 'NONE', #69710, #10997, #72270 ) ;
#135763=ADVANCED_FACE ( 'NONE', ( #63635 ), #243554, .T. ) ;
#135813=ORIENTED_EDGE ( 'NONE', *, *, #215503, .F. ) ;
#136093=DIRECTION ( 'NONE',  ( 1.000000000000000000, -4.851622311275597861E-17, 1.082981191754466620E-16 ) ) ;
#136123=VECTOR ( 'NONE', #177361, 1000.000000000000114 ) ;
#136201=CARTESIAN_POINT ( 'NONE',  ( 14.45204356427542614, 46.53494637834451453, -234.7711487335851928 ) ) ;
#136212=CARTESIAN_POINT ( 'NONE',  ( -16.87036670365548474, 51.65495115403913218, -231.7824289814309111 ) ) ;
#136312=CARTESIAN_POINT ( 'NONE',  ( -16.83233564386407366, 51.51243561217257394, -232.0158193348888744 ) ) ;
#136332=CARTESIAN_POINT ( 'NONE',  ( -16.92209698673563878, 51.56352646095744774, -231.9712590729939734 ) ) ;
#136372=ORIENTED_EDGE ( 'NONE', *, *, #3794, .T. ) ;
#136517=ORIENTED_EDGE ( 'NONE', *, *, #243538, .T. ) ;
#136709=DIRECTION ( 'NONE',  ( 0.000000000000000000, -0.9126074666063770380, -0.4088369013363281068 ) ) ;
#136969=CARTESIAN_POINT ( 'NONE',  ( -18.35235881385853318, 40.40978641300705476, -235.2986935099420975 ) ) ;
#137075=EDGE_CURVE ( 'NONE', #181396, #115352, #197886, .T. ) ;
#137179=ORIENTED_EDGE ( 'NONE', *, *, #150682, .T. ) ;
#137370=DIRECTION ( 'NONE',  ( -1.000000000000000000, -0.000000000000000000, 0.000000000000000000 ) ) ;
#137494=VECTOR ( 'NONE', #81967, 1000.000000000000114 ) ;
#137578=CARTESIAN_POINT ( 'NONE',  ( 12.26145404764308644, 48.33210975535352816, -234.0748017065895397 ) ) ;
#137605=CARTESIAN_POINT ( 'NONE',  ( -16.77308656112214891, 51.61868662400122787, -231.9465479995465103 ) ) ;
#137624=EDGE_CURVE ( 'NONE', #148058, #8019, #238194, .T. ) ;
#137682=ADVANCED_FACE ( 'NONE', ( #60982 ), #140512, .F. ) ;
#137716=CARTESIAN_POINT ( 'NONE',  ( -21.65000000000000213, 52.72272256579932304, -234.4105091754867942 ) ) ;
#137904=EDGE_CURVE ( 'NONE', #172948, #162125, #171682, .T. ) ;
#137974=LINE ( 'NONE', #21906, #255770 ) ;
#137989=EDGE_CURVE ( 'NONE', #68795, #2625, #251160, .T. ) ;
#138068=CARTESIAN_POINT ( 'NONE',  ( 16.27683809663749770, 41.27791846035906786, -237.2365415511148115 ) ) ;
#138137=CARTESIAN_POINT ( 'NONE',  ( -18.38204789744325396, 54.09641185402763597, -229.1605894844069837 ) ) ;
#138277=FACE_BOUND ( 'NONE', #184181, .T. ) ;
#138355=VECTOR ( 'NONE', #116158, 1000.000000000000114 ) ;
#138422=CARTESIAN_POINT ( 'NONE',  ( -21.64999999999999858, 51.48671849539696410, -231.8960919591225718 ) ) ;
#138844=CARTESIAN_POINT ( 'NONE',  ( 15.74999999999999645, 48.12247445990688988, -234.1702647910923361 ) ) ;
#139011=CARTESIAN_POINT ( 'NONE',  ( -16.89060415895971090, 44.13125937934476184, -235.2994854922266370 ) ) ;
#139110=CARTESIAN_POINT ( 'NONE',  ( 18.54999999999999716, 44.62608598762252399, -236.3940605665350745 ) ) ;
#139186=CARTESIAN_POINT ( 'NONE',  ( -12.47155713865592830, 47.30686838571506314, -234.5075185885025633 ) ) ;
#139492=CARTESIAN_POINT ( 'NONE',  ( -16.89318236219977010, 51.62291660267955962, -231.9429707449544082 ) ) ;
#139980=DIRECTION ( 'NONE',  ( -0.000000000000000000, 0.9126074666063770380, 0.4088369013363281068 ) ) ;
#140292=EDGE_LOOP ( 'NONE', ( #26655, #35499, #13247, #136517 ) ) ;
#140509=CARTESIAN_POINT ( 'NONE',  ( -18.39999999999999858, 40.43017315096746955, -235.2838021754311058 ) ) ;
#140512=PLANE ( 'NONE',  #92633 ) ;
#140572=CARTESIAN_POINT ( 'NONE',  ( -18.40000000000000213, 54.05352898164365882, -229.1867466607862127 ) ) ;
#140646=PLANE ( 'NONE',  #26850 ) ;
#140864=DIRECTION ( 'NONE',  ( 1.186688945009010077E-16, 0.4088369013363280513, -0.9126074666063769270 ) ) ;
#140888=CARTESIAN_POINT ( 'NONE',  ( -16.92778301347103920, 44.04299733248424076, -235.2845399950809906 ) ) ;
#140936=DIRECTION ( 'NONE',  ( 0.000000000000000000, -0.4088369013363281068, 0.9126074666063769270 ) ) ;
#141129=CARTESIAN_POINT ( 'NONE',  ( -16.81744102076749314, 44.13548170601895038, -235.2989316066074821 ) ) ;
#141240=LINE ( 'NONE', #57826, #61628 ) ;
#141469=CARTESIAN_POINT ( 'NONE',  ( -16.89146115310546037, 51.62267385565390043, -231.9431803160651384 ) ) ;
#141532=DIRECTION ( 'NONE',  ( 1.073024830501117923E-15, -0.9126074666063771490, -0.4088369013363281623 ) ) ;
#141622=CARTESIAN_POINT ( 'NONE',  ( -17.04295772865321368, 44.10486005708381185, -235.2305778318707326 ) ) ;
#141754=EDGE_CURVE ( 'NONE', #14805, #213760, #70133, .T. ) ;
#141939=SHAPE_REPRESENTATION ( 'Snap Open Cable Crossbars 9', ( #2425 ), #222606 ) ;
#142184=EDGE_LOOP ( 'NONE', ( #80820, #25111, #93793 ) ) ;
#142323=ORIENTED_EDGE ( 'NONE', *, *, #137904, .F. ) ;
#142492=CARTESIAN_POINT ( 'NONE',  ( 17.74533788810830615, 41.64821155081010318, -235.4615294780919896 ) ) ;
#142508=DIRECTION ( 'NONE',  ( 0.000000000000000000, -0.9126074666063770380, -0.4088369013363281068 ) ) ;
#142619=DIRECTION ( 'NONE',  ( -1.020425574104004394E-15, 0.9126074666063769270, 0.4088369013363280513 ) ) ;
#142760=CARTESIAN_POINT ( 'NONE',  ( 20.73486653747090003, 52.72272256579930172, -234.4105091754867658 ) ) ;
#142905=ORIENTED_EDGE ( 'NONE', *, *, #93427, .F. ) ;
#143042=CARTESIAN_POINT ( 'NONE',  ( 15.74999999999999645, 47.91805600923871822, -233.7139610577891631 ) ) ;
#143282=CIRCLE ( 'NONE', #184985, 1.749999999999998002 ) ;
#143350=CARTESIAN_POINT ( 'NONE',  ( -16.87036670365548474, 51.72098459467785858, -231.8575261499355520 ) ) ;
#143434=CARTESIAN_POINT ( 'NONE',  ( -16.92507428761701505, 44.19333870103346129, -235.2730123856632076 ) ) ;
#143787=VERTEX_POINT ( 'NONE', #91217 ) ;
#143873=CIRCLE ( 'NONE', #48026, 14.20833333333334281 ) ;
#143911=EDGE_CURVE ( 'NONE', #13111, #159544, #167901, .T. ) ;
#143915=DIRECTION ( 'NONE',  ( 1.000000000000000000, 9.312479980434134033E-16, 4.171876297610248080E-16 ) ) ;
#143926=VECTOR ( 'NONE', #198628, 1000.000000000000114 ) ;
#144098=ORIENTED_EDGE ( 'NONE', *, *, #3202, .T. ) ;
#144173=CARTESIAN_POINT ( 'NONE',  ( -16.97092634996807448, 44.09655455895979514, -235.2606083258442311 ) ) ;
#144479=CARTESIAN_POINT ( 'NONE',  ( 20.05000000000002913, 42.13647595316533767, -239.1530172309881550 ) ) ;
#144497=VERTEX_POINT ( 'NONE', #168890 ) ;
#144502=ORIENTED_EDGE ( 'NONE', *, *, #21489, .T. ) ;
#145383=CARTESIAN_POINT ( 'NONE',  ( 20.99999999999999645, 44.21724908628621620, -235.4814530999287285 ) ) ;
#145441=LINE ( 'NONE', #8517, #79701 ) ;
#145469=ORIENTED_EDGE ( 'NONE', *, *, #241866, .T. ) ;
#145593=CARTESIAN_POINT ( 'NONE',  ( -16.93301857435215396, 51.64075575048902778, -231.9078325284192204 ) ) ;
#145679=CARTESIAN_POINT ( 'NONE',  ( -17.29838795459091116, 52.59160405768363233, -231.0487749297699622 ) ) ;
#145707=CARTESIAN_POINT ( 'NONE',  ( -16.81453046979152433, 44.19626918183404030, -235.2836408652933642 ) ) ;
#145832=LINE ( 'NONE', #225366, #83396 ) ;
#145842=AXIS2_PLACEMENT_3D ( 'NONE', #255182, #14084, #154895 ) ;
#145932=CARTESIAN_POINT ( 'NONE',  ( -21.65000000000000213, 51.52760218553059701, -231.9873527057832234 ) ) ;
#145974=CARTESIAN_POINT ( 'NONE',  ( -17.11825945287481332, 51.57797924205760864, -231.8552082689889460 ) ) ;
#146165=DIRECTION ( 'NONE',  ( 0.000000000000000000, -0.4088369013363281068, 0.9126074666063770380 ) ) ;
#146606=EDGE_CURVE ( 'NONE', #165639, #68414, #25011, .T. ) ;
#146644=DIRECTION ( 'NONE',  ( 1.073024830501117923E-15, 0.9126074666063771490, 0.4088369013363281623 ) ) ;
#146752=EDGE_CURVE ( 'NONE', #74012, #157279, #145832, .T. ) ;
#146884=UNCERTAINTY_MEASURE_WITH_UNIT (LENGTH_MEASURE( 1.000000000000000082E-05 ), #123024, 'distance_accuracy_value', 'NONE');
#146988=CARTESIAN_POINT ( 'NONE',  ( -16.77683809663752257, 44.14991418685006153, -235.2970290647049580 ) ) ;
#147275=CARTESIAN_POINT ( 'NONE',  ( -16.83199318825829138, 51.51505883799278251, -232.0141791960918738 ) ) ;
#147386=EDGE_LOOP ( 'NONE', ( #174661, #251163, #222550, #179769 ) ) ;
#147414=EDGE_CURVE ( 'NONE', #120740, #181396, #6461, .T. ) ;
#147484=VECTOR ( 'NONE', #60052, 1000.000000000000114 ) ;
#147532=CARTESIAN_POINT ( 'NONE',  ( 18.54999999999999716, 52.10946721379481517, -233.0415979755771900 ) ) ;
#147814=CARTESIAN_POINT ( 'NONE',  ( 23.24999999999999645, 53.37686160793744250, -235.8706811220569932 ) ) ;
#147875=ORIENTED_EDGE ( 'NONE', *, *, #223299, .T. ) ;
#148058=VERTEX_POINT ( 'NONE', #159802 ) ;
#148077=CARTESIAN_POINT ( 'NONE',  ( 23.24999999999999645, 41.49355468354239207, -237.7178856438439141 ) ) ;
#148170=CARTESIAN_POINT ( 'NONE',  ( -16.94445028196807002, 51.64060657411747712, -231.8906364537310196 ) ) ;
#148298=CARTESIAN_POINT ( 'NONE',  ( -16.87372386987899375, 44.61949230436924552, -235.1581464042268408 ) ) ;
#148541=CARTESIAN_POINT ( 'NONE',  ( -16.77732147262506146, 51.60818360671130733, -231.9556725012951119 ) ) ;
#148580=AXIS2_PLACEMENT_3D ( 'NONE', #127038, #50066, #7080 ) ;
#148738=ADVANCED_FACE ( 'NONE', ( #163998 ), #229885, .F. ) ;
#148835=PRODUCT_DEFINITION ( 'UNKNOWN', '', #190452, #243437 ) ;
#149180=CARTESIAN_POINT ( 'NONE',  ( -18.41431012584568094, 40.38283566019376281, -235.2953683571930412 ) ) ;
#149232=( BOUNDED_CURVE ( )  B_SPLINE_CURVE ( 3, ( #169769, #167195, #108470, #129317 ),
 .UNSPECIFIED., .F., .F. ) 
 B_SPLINE_CURVE_WITH_KNOTS ( ( 4, 4 ),
 ( 4.336808689942047397E-14, 1.570796326794915432 ),
 .UNSPECIFIED. ) 
 CURVE ( )  GEOMETRIC_REPRESENTATION_ITEM ( )  RATIONAL_B_SPLINE_CURVE ( ( 1.000000000000000000, 0.8047378541243708217, 0.8047378541243708217, 1.000000000000000000 ) ) 
 REPRESENTATION_ITEM ( '' )  );
#149498=ORIENTED_EDGE ( 'NONE', *, *, #31614, .T. ) ;
#149584=CARTESIAN_POINT ( 'NONE',  ( -16.82055514392434148, 44.15993782893624342, -235.2879755648503703 ) ) ;
#149865=CARTESIAN_POINT ( 'NONE',  ( -16.87683809663752399, 50.97313360171294505, -232.3453239361865315 ) ) ;
#150070=VERTEX_POINT ( 'NONE', #151224 ) ;
#150183=ORIENTED_EDGE ( 'NONE', *, *, #150943, .F. ) ;
#150191=CARTESIAN_POINT ( 'NONE',  ( -18.40000000000000213, 54.02969457822032950, -229.1974241798695004 ) ) ;
#150247=DIRECTION ( 'NONE',  ( 1.000000000000000000, 0.000000000000000000, 0.000000000000000000 ) ) ;
#150672=CARTESIAN_POINT ( 'NONE',  ( 13.88302573338719625, 46.48157447062519765, -234.7876710066568648 ) ) ;
#150682=EDGE_CURVE ( 'NONE', #230513, #148058, #199987, .T. ) ;
#150698=CARTESIAN_POINT ( 'NONE',  ( -16.86337532320261090, 51.69689044229821917, -231.8786767479558080 ) ) ;
#150794=FACE_OUTER_BOUND ( 'NONE', #73968, .T. ) ;
#150840=CARTESIAN_POINT ( 'NONE',  ( -16.80070461187950315, 44.13271087384504199, -235.3001729052809026 ) ) ;
#150906=EDGE_CURVE ( 'NONE', #151483, #183570, #174262, .T. ) ;
#150943=EDGE_CURVE ( 'NONE', #68414, #32277, #178958, .T. ) ;
#151069=CARTESIAN_POINT ( 'NONE',  ( 20.27550659511088682, 44.43555011622476769, -235.9687455856084739 ) ) ;
#151144=CARTESIAN_POINT ( 'NONE',  ( -16.85312964099710342, 51.40816044925842476, -232.0807417151861500 ) ) ;
#151224=CARTESIAN_POINT ( 'NONE',  ( -16.87683809663752399, 44.86297841676450560, -235.0825981793917947 ) ) ;
#151355=CYLINDRICAL_SURFACE ( 'NONE', #71712, 1.749999999999998002 ) ;
#151483=VERTEX_POINT ( 'NONE', #230588 ) ;
#151488=CARTESIAN_POINT ( 'NONE',  ( -18.40000000000000213, 43.51275691321468742, -233.9088826807484622 ) ) ;
#151537=PLANE ( 'NONE',  #74325 ) ;
#151684=VECTOR ( 'NONE', #171756, 1000.000000000000000 ) ;
#151744=ORIENTED_EDGE ( 'NONE', *, *, #226859, .T. ) ;
#151841=FILL_AREA_STYLE ('',( #172713 ) ) ;
#151933=( GEOMETRIC_REPRESENTATION_CONTEXT ( 3 ) GLOBAL_UNCERTAINTY_ASSIGNED_CONTEXT ( ( #146884 ) ) GLOBAL_UNIT_ASSIGNED_CONTEXT ( ( #123024, #78729, #222079 ) ) REPRESENTATION_CONTEXT ( 'NONE', 'WORKASPACE' ) );
#152128=ORIENTED_EDGE ( 'NONE', *, *, #71226, .T. ) ;
#152370=AXIS2_PLACEMENT_3D ( 'NONE', #255615, #140864, #178737 ) ;
#152419=VECTOR ( 'NONE', #4971, 1000.000000000000114 ) ;
#152809=VECTOR ( 'NONE', #176357, 1000.000000000000114 ) ;
#152813=EDGE_CURVE ( 'NONE', #8019, #148058, #65294, .T. ) ;
#152864=VERTEX_POINT ( 'NONE', #143042 ) ;
#153194=ORIENTED_EDGE ( 'NONE', *, *, #124755, .T. ) ;
#153339=CYLINDRICAL_SURFACE ( 'NONE', #37237, 0.1999999999999987899 ) ;
#153358=ORIENTED_EDGE ( 'NONE', *, *, #198016, .F. ) ;
#153387=CARTESIAN_POINT ( 'NONE',  ( -16.82055514392346396, 51.59440680927360745, -231.9574250574065957 ) ) ;
#153449=CARTESIAN_POINT ( 'NONE',  ( -16.93226657140833069, 44.05016941585932244, -235.2828622548803708 ) ) ;
#153513=CARTESIAN_POINT ( 'NONE',  ( 0.000000000000000000, 0.000000000000000000, 0.000000000000000000 ) ) ;
#153594=ORIENTED_EDGE ( 'NONE', *, *, #88674, .F. ) ;
#153706=CARTESIAN_POINT ( 'NONE',  ( -15.70407651835960650, 47.70130725485975631, -234.3525798712488779 ) ) ;
#153751=ORIENTED_EDGE ( 'NONE', *, *, #89824, .T. ) ;
#153782=EDGE_CURVE ( 'NONE', #212682, #211698, #25042, .T. ) ;
#154290=CARTESIAN_POINT ( 'NONE',  ( -16.94226253665224746, 51.34806072463185700, -232.0677850682404255 ) ) ;
#154305=DIRECTION ( 'NONE',  ( 1.000000000000000000, 0.000000000000000000, 0.000000000000000000 ) ) ;
#154554=CARTESIAN_POINT ( 'NONE',  ( 12.93225390519045881, 46.82518482938920101, -234.6773041598981990 ) ) ;
#154656=CARTESIAN_POINT ( 'NONE',  ( -16.77180007708460963, 51.63199159464676313, -231.9405875366200860 ) ) ;
#154884=CARTESIAN_POINT ( 'NONE',  ( 23.24999999999999645, 40.29670989715187090, -235.0462836312595130 ) ) ;
#154895=DIRECTION ( 'NONE',  ( 0.000000000000000000, -0.9126074666063769270, -0.4088369013363280513 ) ) ;
#155188=EDGE_CURVE ( 'NONE', #57171, #64755, #233923, .T. ) ;
#155294=ORIENTED_EDGE ( 'NONE', *, *, #239869, .F. ) ;
#155344=CARTESIAN_POINT ( 'NONE',  ( -16.89318236219975944, 44.13017269538578091, -235.2996277017026046 ) ) ;
#155569=EDGE_CURVE ( 'NONE', #212622, #167295, #16655, .T. ) ;
#155587=B_SPLINE_CURVE_WITH_KNOTS ( 'NONE', 3,
 ( #69225, #228283, #49631, #138137, #116045, #78168, #177323 ),
 .UNSPECIFIED., .F., .F.,
 ( 4, 3, 4 ),
 ( 0.000000000000000000, 3.882884552233767958E-05, 5.798605692157499417E-05 ),
 .UNSPECIFIED. ) ;
#155677=ORIENTED_EDGE ( 'NONE', *, *, #98572, .T. ) ;
#155825=CARTESIAN_POINT ( 'NONE',  ( 15.70340296795548163, 47.69902910524211137, -234.3535107520372947 ) ) ;
#155938=CARTESIAN_POINT ( 'NONE',  ( -16.97683809663752186, 50.93224991157929793, -232.2540631895259082 ) ) ;
#155958=CARTESIAN_POINT ( 'NONE',  ( -16.91049119928364775, 51.64781119986088243, -231.9335005483882810 ) ) ;
#156035=CIRCLE ( 'NONE', #226740, 1.500000000000001332 ) ;
#156242=CARTESIAN_POINT ( 'NONE',  ( -13.43673303185028800, 46.56726880910646571, -234.7610735323249571 ) ) ;
#156424=( BOUNDED_CURVE ( )  B_SPLINE_CURVE ( 3, ( #121351, #143434, #46888, #44353 ),
 .UNSPECIFIED., .F., .T. ) 
 B_SPLINE_CURVE_WITH_KNOTS ( ( 4, 4 ),
 ( 0.5235987755983111391, 1.570796326794896558 ),
 .UNSPECIFIED. ) 
 CURVE ( )  GEOMETRIC_REPRESENTATION_ITEM ( )  RATIONAL_B_SPLINE_CURVE ( ( 1.000000000000000000, 0.9106836025229610998, 0.9106836025229610998, 1.000000000000000000 ) ) 
 REPRESENTATION_ITEM ( '' )  );
#156474=EDGE_LOOP ( 'NONE', ( #41740, #65635, #177497, #36640, #41284 ) ) ;
#156594=LINE ( 'NONE', #134396, #138355 ) ;
#156634=CARTESIAN_POINT ( 'NONE',  ( -16.90202395485720288, 44.08058226997761153, -235.3060544617264327 ) ) ;
#156660=VERTEX_POINT ( 'NONE', #255540 ) ;
#156686=ORIENTED_EDGE ( 'NONE', *, *, #65177, .T. ) ;
#157027=ADVANCED_BREP_SHAPE_REPRESENTATION ( '', ( #21402, #2425 ), #222606 ) ;
#157194=CARTESIAN_POINT ( 'NONE',  ( 15.57250062127603663, 48.82262352862032628, -233.8339354177745690 ) ) ;
#157245=CARTESIAN_POINT ( 'NONE',  ( -17.01764560440449614, 51.52760218624815991, -231.9873527054617455 ) ) ;
#157279=VERTEX_POINT ( 'NONE', #45217 ) ;
#157539=CARTESIAN_POINT ( 'NONE',  ( -12.25000000000000533, 47.91126876242805110, -234.2648823414209289 ) ) ;
#157573=CARTESIAN_POINT ( 'NONE',  ( -15.51798037960204724, 48.91301996986818068, -233.7868972119375428 ) ) ;
#158118=CARTESIAN_POINT ( 'NONE',  ( 23.04999999999999716, 52.07980129617636322, -232.9753775883424964 ) ) ;
#158369=ADVANCED_FACE ( 'NONE', ( #220467 ), #241313, .F. ) ;
#158479=CARTESIAN_POINT ( 'NONE',  ( 12.33938619321247110, 48.63273434562352548, -233.9299239298080124 ) ) ;
#158498=CARTESIAN_POINT ( 'NONE',  ( -16.87331047859649757, 51.61886293219124155, -231.9464690156495692 ) ) ;
#158512=DIRECTION ( 'NONE',  ( 0.000000000000000000, -0.9126074666063769270, -0.4088369013363280513 ) ) ;
#158552=CARTESIAN_POINT ( 'NONE',  ( -18.40000000000000213, 54.02969457822032950, -229.1974241798695004 ) ) ;
#158662=ORIENTED_EDGE ( 'NONE', *, *, #132905, .T. ) ;
#158698=FACE_OUTER_BOUND ( 'NONE', #227879, .T. ) ;
#158705=ORIENTED_EDGE ( 'NONE', *, *, #9065, .F. ) ;
#158773=DIRECTION ( 'NONE',  ( -1.000000000000000000, 0.000000000000000000, 0.000000000000000000 ) ) ;
#158873=CARTESIAN_POINT ( 'NONE',  ( -16.77828822508139694, 44.14854791318649774, -235.2972098120475266 ) ) ;
#158982=AXIS2_PLACEMENT_3D ( 'NONE', #126368, #205898, #106792 ) ;
#159096=CARTESIAN_POINT ( 'NONE',  ( -16.94878442675512886, 51.63668200512650230, -231.8927611518110155 ) ) ;
#159189=CARTESIAN_POINT ( 'NONE',  ( -16.92973740335530053, 44.06694468412165122, -235.2830613104084421 ) ) ;
#159477=VERTEX_POINT ( 'NONE', #107276 ) ;
#159544=VERTEX_POINT ( 'NONE', #173416 ) ;
#159577=ORIENTED_EDGE ( 'NONE', *, *, #147414, .T. ) ;
#159595=VECTOR ( 'NONE', #227333, 1000.000000000000114 ) ;
#159740=CARTESIAN_POINT ( 'NONE',  ( 13.88638282980484107, 49.67565583792541162, -233.3567449137544543 ) ) ;
#159802=CARTESIAN_POINT ( 'NONE',  ( -12.25000000000000178, 48.12247445990688988, -234.1702647910923361 ) ) ;
#159973=DIRECTION ( 'NONE',  ( -1.000000000000000000, 6.731126513909287799E-15, -1.502524917684071019E-14 ) ) ;
#160192=CARTESIAN_POINT ( 'NONE',  ( -33.72168855820451938, 44.13548170601888643, -235.2989316066074821 ) ) ;
#160344=PRODUCT_CONTEXT ( 'NONE', #203932, 'mechanical' ) ;
#160464=CARTESIAN_POINT ( 'NONE',  ( -33.72168855820452649, 42.27269979661959098, -221.1123729563994402 ) ) ;
#160504=ORIENTED_EDGE ( 'NONE', *, *, #141754, .T. ) ;
#160640=ORIENTED_EDGE ( 'NONE', *, *, #129180, .F. ) ;
#160771=FACE_OUTER_BOUND ( 'NONE', #83789, .T. ) ;
#160780=ORIENTED_EDGE ( 'NONE', *, *, #35886, .T. ) ;
#160822=CARTESIAN_POINT ( 'NONE',  ( 20.09999999999999787, 41.11438369982452912, -236.8714985644722617 ) ) ;
#160876=FILL_AREA_STYLE ('',( #121751 ) ) ;
#161030=CARTESIAN_POINT ( 'NONE',  ( 12.68104795156995301, 49.15836891943283860, -233.6552066833104107 ) ) ;
#161120=ORIENTED_EDGE ( 'NONE', *, *, #31614, .F. ) ;
#161329=AXIS2_PLACEMENT_3D ( 'NONE', #109265, #188814, #248804 ) ;
#161451=CARTESIAN_POINT ( 'NONE',  ( -18.40000000000000213, 54.07421472284888608, -229.1714396514910561 ) ) ;
#161475=CARTESIAN_POINT ( 'NONE',  ( -16.92925196614877237, 44.09600274329658021, -235.2921473758737818 ) ) ;
#161515=ADVANCED_FACE ( 'NONE', ( #55363 ), #223449, .F. ) ;
#161973=VECTOR ( 'NONE', #246325, 1000.000000000000114 ) ;
#162125=VERTEX_POINT ( 'NONE', #93309 ) ;
#162163=( NAMED_UNIT ( * ) SI_UNIT ( $, .STERADIAN. ) SOLID_ANGLE_UNIT ( ) );
#162212=CARTESIAN_POINT ( 'NONE',  ( 23.04999999999999716, 41.49355468354239207, -237.7178856438439141 ) ) ;
#162327=CIRCLE ( 'NONE', #74866, 0.09999999999999609201 ) ;
#162355=FACE_OUTER_BOUND ( 'NONE', #168589, .T. ) ;
#162361=EDGE_CURVE ( 'NONE', #64755, #107188, #44588, .T. ) ;
#162365=DIRECTION ( 'NONE',  ( 1.000000000000000000, -7.710376986078650754E-15, 1.458655703008169508E-14 ) ) ;
#162878=VERTEX_POINT ( 'NONE', #8993 ) ;
#163126=DIRECTION ( 'NONE',  ( -0.5932847527679298016, -0.3291107096594080295, 0.7346423231209709970 ) ) ;
#163383=DIRECTION ( 'NONE',  ( 1.186688945009010077E-16, 0.4088369013363281623, -0.9126074666063771490 ) ) ;
#163614=CARTESIAN_POINT ( 'NONE',  ( -16.88853107394619357, 51.62118350788017551, -231.9444668182231339 ) ) ;
#163693=VERTEX_POINT ( 'NONE', #90474 ) ;
#163742=VECTOR ( 'NONE', #232931, 1000.000000000000000 ) ;
#163767=CARTESIAN_POINT ( 'NONE',  ( -17.11825945287483108, 44.13548170601893617, -235.2989316066074252 ) ) ;
#163818=AXIS2_PLACEMENT_3D ( 'NONE', #121605, #81143, #223224 ) ;
#163832=EDGE_CURVE ( 'NONE', #212622, #28415, #133421, .T. ) ;
#163998=FACE_OUTER_BOUND ( 'NONE', #222924, .T. ) ;
#164083=CARTESIAN_POINT ( 'NONE',  ( 22.88900146558018989, 41.54206602352874000, -237.8261728628838512 ) ) ;
#164110=PLANE ( 'NONE',  #95595 ) ;
#164342=DIRECTION ( 'NONE',  ( 0.000000000000000000, 0.4088369013363281068, -0.9126074666063770380 ) ) ;
#164379=VECTOR ( 'NONE', #136709, 1000.000000000000114 ) ;
#164391=CARTESIAN_POINT ( 'NONE',  ( 18.39999999999999503, 53.37686160793744961, -235.8706811220569932 ) ) ;
#164541=DIRECTION ( 'NONE',  ( 0.000000000000000000, 0.4088369013363281068, -0.9126074666063770380 ) ) ;
#164545=CARTESIAN_POINT ( 'NONE',  ( -16.92989143108098204, 44.34764822598747713, -235.2038836196412603 ) ) ;
#164592=ORIENTED_EDGE ( 'NONE', *, *, #187158, .F. ) ;
#164599=DIRECTION ( 'NONE',  ( -1.000000000000000000, -0.000000000000000000, -0.000000000000000000 ) ) ;
#164758=DIRECTION ( 'NONE',  ( 0.000000000000000000, -0.9126074666063770380, -0.4088369013363281068 ) ) ;
#165043=FACE_OUTER_BOUND ( 'NONE', #189205, .T. ) ;
#165135=DIRECTION ( 'NONE',  ( 0.000000000000000000, -0.4088369013363281068, 0.9126074666063770380 ) ) ;
#165381=EDGE_LOOP ( 'NONE', ( #134128, #71169, #191958, #66543 ) ) ;
#165510=CARTESIAN_POINT ( 'NONE',  ( -18.40000000000000213, 53.37686160793744961, -235.8706811220569932 ) ) ;
#165639=VERTEX_POINT ( 'NONE', #112076 ) ;
#165676=DIRECTION ( 'NONE',  ( 0.000000000000000000, -0.4088369013363281068, 0.9126074666063770380 ) ) ;
#166041=EDGE_CURVE ( 'NONE', #225390, #7237, #198665, .T. ) ;
#166845=CARTESIAN_POINT ( 'NONE',  ( -15.75000000000000355, 47.91805600923872532, -233.7139610577891631 ) ) ;
#166949=ADVANCED_FACE ( 'NONE', ( #81920 ), #140646, .F. ) ;
#167062=EDGE_CURVE ( 'NONE', #202918, #210551, #49252, .T. ) ;
#167108=ORIENTED_EDGE ( 'NONE', *, *, #37917, .F. ) ;
#167195=CARTESIAN_POINT ( 'NONE',  ( -18.40000000000000213, 51.03393957836610184, -230.5394855108573040 ) ) ;
#167295=VERTEX_POINT ( 'NONE', #39997 ) ;
#167507=ADVANCED_FACE ( 'NONE', ( #165043 ), #120244, .T. ) ;
#167684=CARTESIAN_POINT ( 'NONE',  ( -16.87331047859649757, 51.61886293219124155, -231.9464690156495692 ) ) ;
#167852=CARTESIAN_POINT ( 'NONE',  ( -16.91256925476569961, 51.71161613007731006, -231.8657639032808504 ) ) ;
#167901=LINE ( 'NONE', #27108, #207447 ) ;
#167904=CARTESIAN_POINT ( 'NONE',  ( -18.40000000000000213, 50.88295650978584206, -230.3037755757580953 ) ) ;
#167988=PLANE ( 'NONE',  #212504 ) ;
#167998=VECTOR ( 'NONE', #150247, 1000.000000000000000 ) ;
#168251=VERTEX_POINT ( 'NONE', #104115 ) ;
#168270=ORIENTED_EDGE ( 'NONE', *, *, #232612, .T. ) ;
#168589=EDGE_LOOP ( 'NONE', ( #187475, #183036, #65110, #33788 ) ) ;
#168693=ORIENTED_EDGE ( 'NONE', *, *, #130729, .T. ) ;
#168776=CARTESIAN_POINT ( 'NONE',  ( -17.29838795455454559, 42.81805030517067223, -235.4272065966908656 ) ) ;
#168890=CARTESIAN_POINT ( 'NONE',  ( -16.87036670365549895, 44.00112830765706917, -235.3159266546824995 ) ) ;
#168919=ORIENTED_EDGE ( 'NONE', *, *, #182521, .T. ) ;
#169144=CARTESIAN_POINT ( 'NONE',  ( -17.78241384943523684, 53.43976629469171513, -230.1384318238924322 ) ) ;
#169182=CARTESIAN_POINT ( 'NONE',  ( 18.54999999999999716, 44.13548170601889353, -235.2989316066074821 ) ) ;
#169278=AXIS2_PLACEMENT_3D ( 'NONE', #78916, #218435, #158512 ) ;
#169421=CARTESIAN_POINT ( 'NONE',  ( -16.77779411440718249, 51.60854050822252503, -231.9553652180356949 ) ) ;
#169453=CARTESIAN_POINT ( 'NONE',  ( -16.81931177881023487, 51.55410748565302725, -231.9897278734257497 ) ) ;
#169594=CARTESIAN_POINT ( 'NONE',  ( -18.40000000000000213, 45.89348038176515843, -239.2231437130149061 ) ) ;
#169769=CARTESIAN_POINT ( 'NONE',  ( -18.40000000000000213, 51.08739888604760182, -230.5155363996569520 ) ) ;
#169800=FACE_OUTER_BOUND ( 'NONE', #247486, .T. ) ;
#169833=DIRECTION ( 'NONE',  ( -1.000000000000000000, -0.000000000000000000, 0.000000000000000000 ) ) ;
#170054=CARTESIAN_POINT ( 'NONE',  ( -16.87036670365549540, 44.00112830765706207, -235.3159266546824995 ) ) ;
#170239=DIRECTION ( 'NONE',  ( -1.000000000000000000, -0.000000000000000000, 0.000000000000000000 ) ) ;
#170307=CARTESIAN_POINT ( 'NONE',  ( -16.88460203013676519, 51.63142026009736441, -231.9356287555948199 ) ) ;
#170498=EDGE_CURVE ( 'NONE', #159544, #68788, #22331, .T. ) ;
#170539=AXIS2_PLACEMENT_3D ( 'NONE', #220883, #61832, #202618 ) ;
#170743=DIRECTION ( 'NONE',  ( 0.000000000000000000, 0.9126074666063769270, 0.4088369013363280513 ) ) ;
#170876=EDGE_LOOP ( 'NONE', ( #184844, #11791, #251120, #241807 ) ) ;
#170939=CARTESIAN_POINT ( 'NONE',  ( -17.11825945287482753, 44.09459801588531036, -235.2076708599468020 ) ) ;
#171001=CARTESIAN_POINT ( 'NONE',  ( 21.72449340488909897, 51.48232928251994167, -231.6416980232910987 ) ) ;
#171549=CARTESIAN_POINT ( 'NONE',  ( 15.06592377766032165, 46.82384836101673642, -234.6777522051880283 ) ) ;
#171650=CARTESIAN_POINT ( 'NONE',  ( -16.97683809663752186, 50.93224991157930504, -232.2540631895259082 ) ) ;
#171682=LINE ( 'NONE', #212073, #163742 ) ;
#171714=CARTESIAN_POINT ( 'NONE',  ( -16.93262454970420094, 44.04387347954221354, -235.2829689446594159 ) ) ;
#171756=DIRECTION ( 'NONE',  ( 1.000000000000000000, 0.000000000000000000, 0.000000000000000000 ) ) ;
#172012=FACE_OUTER_BOUND ( 'NONE', #28328, .T. ) ;
#172022=VERTEX_POINT ( 'NONE', #242363 ) ;
#172110=DIRECTION ( 'NONE',  ( -0.7071067811865457964, -0.2890913453342138228, 0.6453109281988466117 ) ) ;
#172127=( BOUNDED_CURVE ( )  B_SPLINE_CURVE ( 3, ( #59392, #239357, #218480, #123260 ),
 .UNSPECIFIED., .F., .T. ) 
 B_SPLINE_CURVE_WITH_KNOTS ( ( 4, 4 ),
 ( 5.731445031868799056, 5.983100554402348337 ),
 .UNSPECIFIED. ) 
 CURVE ( )  GEOMETRIC_REPRESENTATION_ITEM ( )  RATIONAL_B_SPLINE_CURVE ( ( 1.000000000000000000, 0.9947294176030464508, 0.9947294176030464508, 1.000000000000000000 ) ) 
 REPRESENTATION_ITEM ( '' )  );
#172154=CARTESIAN_POINT ( 'NONE',  ( -18.40000000000000213, 45.89348038176515843, -239.2231437130149061 ) ) ;
#172279=AXIS2_PLACEMENT_3D ( 'NONE', #428, #163383, #64274 ) ;
#172449=ORIENTED_EDGE ( 'NONE', *, *, #227211, .F. ) ;
#172713=FILL_AREA_STYLE_COLOUR ( '', #236409 ) ;
#172948=VERTEX_POINT ( 'NONE', #196782 ) ;
#172950=CARTESIAN_POINT ( 'NONE',  ( -16.87401514999233498, 51.55499682964786246, -231.9750802427320764 ) ) ;
#173416=CARTESIAN_POINT ( 'NONE',  ( 18.39999999999999503, 50.99613813938697149, -230.5564200897905778 ) ) ;
#173776=ORIENTED_EDGE ( 'NONE', *, *, #30916, .T. ) ;
#173784=DIRECTION ( 'NONE',  ( 0.000000000000000000, 0.4088369013363783999, -0.9126074666063545004 ) ) ;
#174157=EDGE_CURVE ( 'NONE', #51518, #8358, #46737, .T. ) ;
#174262=CIRCLE ( 'NONE', #74300, 0.1999999999999987899 ) ;
#174347=EDGE_LOOP ( 'NONE', ( #153194, #7886 ) ) ;
#174549=CARTESIAN_POINT ( 'NONE',  ( -15.39946565075089957, 47.12508421510194268, -234.5737628866445732 ) ) ;
#174661=ORIENTED_EDGE ( 'NONE', *, *, #167062, .F. ) ;
#174966=ORIENTED_EDGE ( 'NONE', *, *, #38611, .F. ) ;
#175520=FACE_OUTER_BOUND ( 'NONE', #241055, .T. ) ;
#175722=ORIENTED_EDGE ( 'NONE', *, *, #89824, .F. ) ;
#175735=CARTESIAN_POINT ( 'NONE',  ( 20.73486653747088582, 45.23934133962701765, -237.7629717664446503 ) ) ;
#175794=CARTESIAN_POINT ( 'NONE',  ( -14.11697426661281440, 46.48157447062519765, -234.7876710066568648 ) ) ;
#175796=DIRECTION ( 'NONE',  ( -0.8049926720990043805, 0.2425566999317304295, -0.5414360951997322369 ) ) ;
#176357=DIRECTION ( 'NONE',  ( 0.000000000000000000, -0.4088369013363281068, 0.9126074666063770380 ) ) ;
#176466=DIRECTION ( 'NONE',  ( 1.000000000000000000, 0.000000000000000000, 0.000000000000000000 ) ) ;
#176480=CARTESIAN_POINT ( 'NONE',  ( -16.87683809663752399, 50.97313360171294505, -232.3453239361865315 ) ) ;
#176785=PLANE ( 'NONE',  #169278 ) ;
#177050=CARTESIAN_POINT ( 'NONE',  ( -23.25000000000000355, 53.98582189624752914, -228.9137301112145622 ) ) ;
#177119=CARTESIAN_POINT ( 'NONE',  ( -15.66061380678752535, 48.63273434562353970, -233.9299239298079840 ) ) ;
#177160=CARTESIAN_POINT ( 'NONE',  ( -16.80438519320023616, 44.13624578021552480, -235.2988313683356409 ) ) ;
#177246=CARTESIAN_POINT ( 'NONE',  ( -16.93211319090181632, 51.66459555148166061, -231.8712077822809761 ) ) ;
#177293=ORIENTED_EDGE ( 'NONE', *, *, #170498, .T. ) ;
#177323=CARTESIAN_POINT ( 'NONE',  ( -18.40000000000000213, 54.09347887257330711, -229.1540424707546322 ) ) ;
#177361=DIRECTION ( 'NONE',  ( -0.000000000000000000, 0.9126074666063770380, 0.4088369013363281068 ) ) ;
#177497=ORIENTED_EDGE ( 'NONE', *, *, #240113, .F. ) ;
#177871=SHAPE_REPRESENTATION_RELATIONSHIP ( 'NONE' , 'NONE' ,  #141939, #157027 ) ;
#177981=ORIENTED_EDGE ( 'NONE', *, *, #66520, .T. ) ;
#178032=CARTESIAN_POINT ( 'NONE',  ( 15.75000000000000000, 48.22810253856975038, -234.1229447132332950 ) ) ;
#178082=CARTESIAN_POINT ( 'NONE',  ( -17.11825945287481687, 51.52760218553060412, -231.9873527057832234 ) ) ;
#178168=DIRECTION ( 'NONE',  ( 1.000000000000000000, -4.851622311275599093E-17, 1.082981191754466866E-16 ) ) ;
#178368=CARTESIAN_POINT ( 'NONE',  ( -13.22483237240078680, 46.65138127958493897, -234.7343221152025023 ) ) ;
#178405=CARTESIAN_POINT ( 'NONE',  ( -12.48127053791144903, 48.91191486804444111, -233.7874788057928868 ) ) ;
#178737=DIRECTION ( 'NONE',  ( 1.000000000000000000, 0.000000000000000000, 0.000000000000000000 ) ) ;
#178766=CARTESIAN_POINT ( 'NONE',  ( -16.92570016628985030, 44.10510403810827995, -235.3029098272679107 ) ) ;
#178844=EDGE_CURVE ( 'NONE', #226785, #68814, #253618, .T. ) ;
#178958=LINE ( 'NONE', #268, #82596 ) ;
#179251=LINE ( 'NONE', #198777, #234223 ) ;
#179339=CARTESIAN_POINT ( 'NONE',  ( -16.87665923198281348, 51.61886293219124155, -231.9464690156495692 ) ) ;
#179488=CARTESIAN_POINT ( 'NONE',  ( -16.87487986503753845, 44.13545556447066076, -235.2989350391281391 ) ) ;
#179671=CARTESIAN_POINT ( 'NONE',  ( -12.92414019175885720, 49.37151442406710800, -233.5366006881135092 ) ) ;
#179769=ORIENTED_EDGE ( 'NONE', *, *, #239869, .T. ) ;
#179817=VECTOR ( 'NONE', #203344, 1000.000000000000000 ) ;
#179934=CARTESIAN_POINT ( 'NONE',  ( -16.94107738177414291, 51.68386028857255354, -231.8469600742508305 ) ) ;
#180313=VECTOR ( 'NONE', #192498, 1000.000000000000114 ) ;
#180339=CARTESIAN_POINT ( 'NONE',  ( -14.00000000000000178, 47.91805600923872532, -233.7139610577891631 ) ) ;
#180359=CARTESIAN_POINT ( 'NONE',  ( 18.39999999999998082, 40.40989152675300033, -235.2989281452919954 ) ) ;
#180383=AXIS2_PLACEMENT_3D ( 'NONE', #106142, #240540, #206549 ) ;
#180433=VECTOR ( 'NONE', #13997, 1000.000000000000114 ) ;
#180585=CARTESIAN_POINT ( 'NONE',  ( 15.07585980824113747, 49.37151442406710089, -233.5366006881135945 ) ) ;
#180757=CARTESIAN_POINT ( 'NONE',  ( -16.87331047859651179, 44.13548170601895038, -235.2989316066074821 ) ) ;
#180870=DIRECTION ( 'NONE',  ( 1.000000000000000000, 0.000000000000000000, 0.000000000000000000 ) ) ;
#180891=EDGE_CURVE ( 'NONE', #157279, #48836, #123710, .T. ) ;
#180947=CARTESIAN_POINT ( 'NONE',  ( -12.25000000000000178, 48.12247445990688988, -234.1702647910923361 ) ) ;
#180980=VECTOR ( 'NONE', #72834, 1000.000000000000114 ) ;
#181013=ORIENTED_EDGE ( 'NONE', *, *, #248678, .T. ) ;
#181222=CARTESIAN_POINT ( 'NONE',  ( -16.91256925476569961, 51.71161613007730296, -231.8657639032808788 ) ) ;
#181236=DIRECTION ( 'NONE',  ( 0.7071067811865457964, 0.2890913453342137673, -0.6453109281988465007 ) ) ;
#181256=ADVANCED_FACE ( 'NONE', ( #27849 ), #4382, .T. ) ;
#181331=EDGE_CURVE ( 'NONE', #77934, #212622, #25263, .T. ) ;
#181384=AXIS2_PLACEMENT_3D ( 'NONE', #119632, #114482, #38808 ) ;
#181396=VERTEX_POINT ( 'NONE', #112501 ) ;
#181410=FACE_OUTER_BOUND ( 'NONE', #140292, .T. ) ;
#181664=PLANE ( 'NONE',  #105562 ) ;
#181683=DIRECTION ( 'NONE',  ( -0.7071067811865463515, 0.2890913453342128236, -0.6453109281988462786 ) ) ;
#181774=FACE_OUTER_BOUND ( 'NONE', #34353, .T. ) ;
#181896=ORIENTED_EDGE ( 'NONE', *, *, #71226, .F. ) ;
#182180=EDGE_CURVE ( 'NONE', #184724, #126269, #10226, .T. ) ;
#182235=CARTESIAN_POINT ( 'NONE',  ( -12.30589683808040391, 48.53345590596380532, -233.9787581418636364 ) ) ;
#182321=DIRECTION ( 'NONE',  ( 0.000000000000000000, 0.4088369013363281068, -0.9126074666063770380 ) ) ;
#182509=FACE_OUTER_BOUND ( 'NONE', #170876, .T. ) ;
#182521=EDGE_CURVE ( 'NONE', #162878, #79207, #202994, .T. ) ;
#182759=DIRECTION ( 'NONE',  ( 0.000000000000000000, 0.9126074666063771490, 0.4088369013363276627 ) ) ;
#182891=LINE ( 'NONE', #5484, #77046 ) ;
#182949=PLANE ( 'NONE',  #86230 ) ;
#182994=DIRECTION ( 'NONE',  ( 1.186688945009010077E-16, 0.4088369013363281068, -0.9126074666063770380 ) ) ;
#183004=SURFACE_STYLE_FILL_AREA ( #160876 ) ;
#183036=ORIENTED_EDGE ( 'NONE', *, *, #234562, .T. ) ;
#183070=ADVANCED_FACE ( 'NONE', ( #217720 ), #76940, .F. ) ;
#183424=LINE ( 'NONE', #247226, #118320 ) ;
#183560=CARTESIAN_POINT ( 'NONE',  ( -16.89935556175728593, 44.58236401100771928, -235.0987338397486326 ) ) ;
#183570=VERTEX_POINT ( 'NONE', #111088 ) ;
#183927=CYLINDRICAL_SURFACE ( 'NONE', #23475, 0.1000000000000024342 ) ;
#183932=CARTESIAN_POINT ( 'NONE',  ( -23.25000000000000355, 53.37686160793744961, -235.8706811220569932 ) ) ;
#184143=CARTESIAN_POINT ( 'NONE',  ( 20.99999999999999645, 41.11438369982452912, -236.8714985644722617 ) ) ;
#184181=EDGE_LOOP ( 'NONE', ( #219040, #113426 ) ) ;
#184219=ORIENTED_EDGE ( 'NONE', *, *, #212162, .F. ) ;
#184270=EDGE_LOOP ( 'NONE', ( #120180, #222772, #29817, #135813, #174966, #207018, #104554, #30245, #18851 ) ) ;
#184482=LINE ( 'NONE', #120698, #40504 ) ;
#184720=CARTESIAN_POINT ( 'NONE',  ( -16.94275863006528482, 51.64076883226000092, -231.8933771982521250 ) ) ;
#184724=VERTEX_POINT ( 'NONE', #190699 ) ;
#184844=ORIENTED_EDGE ( 'NONE', *, *, #19629, .T. ) ;
#184845=ADVANCED_FACE ( 'NONE', ( #39323 ), #38040, .F. ) ;
#184985=AXIS2_PLACEMENT_3D ( 'NONE', #245651, #5724, #42313 ) ;
#185114=CARTESIAN_POINT ( 'NONE',  ( -17.04761207306817994, 51.58760699400681915, -231.8766993777581717 ) ) ;
#185198=VECTOR ( 'NONE', #162365, 1000.000000000000000 ) ;
#185501=ORIENTED_EDGE ( 'NONE', *, *, #137624, .F. ) ;
#185645=B_SPLINE_CURVE_WITH_KNOTS ( 'NONE', 3,
 ( #190155, #251393, #51890, #11521, #111907, #87172, #208446, #227988, #109301, #229279 ),
 .UNSPECIFIED., .F., .F.,
 ( 4, 3, 3, 4 ),
 ( 0.000000000000000000, 4.874959354401955399E-05, 9.785140065120999852E-05, 0.0001360444631936036581 ),
 .UNSPECIFIED. ) ;
#185801=ORIENTED_EDGE ( 'NONE', *, *, #122873, .T. ) ;
#185958=EDGE_CURVE ( 'NONE', #211698, #143787, #110097, .T. ) ;
#186511=LINE ( 'NONE', #183932, #94351 ) ;
#186720=AXIS2_PLACEMENT_3D ( 'NONE', #90106, #109672, #92683 ) ;
#186804=CARTESIAN_POINT ( 'NONE',  ( -17.01825945287481545, 51.52760218553060412, -231.9873527057832234 ) ) ;
#187158=EDGE_CURVE ( 'NONE', #12028, #38227, #219465, .T. ) ;
#187417=CARTESIAN_POINT ( 'NONE',  ( -16.85722902420148372, 44.24093119332965074, -235.2516915354734692 ) ) ;
#187432=CARTESIAN_POINT ( 'NONE',  ( -16.83199030136658436, 44.25509759139306709, -235.2665503012579507 ) ) ;
#187475=ORIENTED_EDGE ( 'NONE', *, *, #37917, .T. ) ;
#187604=B_SPLINE_CURVE_WITH_KNOTS ( 'NONE', 3,
 ( #239637, #60980, #140509, #41452 ),
 .UNSPECIFIED., .F., .F.,
 ( 4, 4 ),
 ( 0.000000000000000000, 7.713889350929889021E-05 ),
 .UNSPECIFIED. ) ;
#187710=CARTESIAN_POINT ( 'NONE',  ( -16.78493211734302903, 51.60783545504983039, -231.9559722212414385 ) ) ;
#188535=CARTESIAN_POINT ( 'NONE',  ( -16.86420534634261514, 51.67279902237199707, -231.8997167030369155 ) ) ;
#188666=CARTESIAN_POINT ( 'NONE',  ( -16.87036670365548474, 51.72098459467786569, -231.8575261499355236 ) ) ;
#188699=CARTESIAN_POINT ( 'NONE',  ( -16.85312841634288716, 44.37593289069839386, -235.2310913830144443 ) ) ;
#188814=DIRECTION ( 'NONE',  ( 1.073024830501117923E-15, 0.9126074666063771490, 0.4088369013363281623 ) ) ;
#188818=ORIENTED_EDGE ( 'NONE', *, *, #2964, .T. ) ;
#189205=EDGE_LOOP ( 'NONE', ( #50858, #247132, #109687, #111072, #256876 ) ) ;
#189310=CARTESIAN_POINT ( 'NONE',  ( -16.94107738177414291, 51.68386028857255354, -231.8469600742508021 ) ) ;
#189494=CARTESIAN_POINT ( 'NONE',  ( -16.77683809663752257, 51.60783545504968117, -231.9559722212415522 ) ) ;
#189549=CARTESIAN_POINT ( 'NONE',  ( 13.99999999999999822, 47.91805600923871822, -233.7139610577891631 ) ) ;
#189634=EDGE_CURVE ( 'NONE', #144497, #181396, #61069, .T. ) ;
#190004=CARTESIAN_POINT ( 'NONE',  ( 20.09999999999999787, 51.70063031245850738, -232.1289905089708441 ) ) ;
#190155=CARTESIAN_POINT ( 'NONE',  ( -16.87036670365549895, 44.00112830765706917, -235.3159266546824995 ) ) ;
#190278=EDGE_LOOP ( 'NONE', ( #172449, #96956, #152128, #227711, #61333 ) ) ;
#190321=EDGE_CURVE ( 'NONE', #32277, #50660, #200839, .T. ) ;
#190452=PRODUCT_DEFINITION_FORMATION_WITH_SPECIFIED_SOURCE ( 'ANY', '', #74532, .NOT_KNOWN. ) ;
#190564=VECTOR ( 'NONE', #205824, 1000.000000000000114 ) ;
#190659=ORIENTED_EDGE ( 'NONE', *, *, #21175, .T. ) ;
#190699=CARTESIAN_POINT ( 'NONE',  ( 23.24999999999999645, 43.39957528361355799, -233.6562381667159798 ) ) ;
#190940=VECTOR ( 'NONE', #6999, 1000.000000000000114 ) ;
#190946=B_SPLINE_CURVE_WITH_KNOTS ( 'NONE', 3,
 ( #158498, #179339, #222262, #61944, #237992, #163614, #82743, #141469, #121923, #22838 ),
 .UNSPECIFIED., .F., .F.,
 ( 4, 3, 3, 4 ),
 ( 0.000000000000000000, 1.004626015990891703E-05, 1.831183478181717294E-05, 2.062343583994978553E-05 ),
 .UNSPECIFIED. ) ;
#191134=CARTESIAN_POINT ( 'NONE',  ( -16.86578989773640558, 51.70927543259747949, -231.8678220941709753 ) ) ;
#191272=CARTESIAN_POINT ( 'NONE',  ( -16.93909480342659890, 44.07255599751472630, -235.2799179410861541 ) ) ;
#191281=CARTESIAN_POINT ( 'NONE',  ( -18.40000000000000213, 51.08739888604760182, -230.5155363996569520 ) ) ;
#191303=EDGE_CURVE ( 'NONE', #69236, #248676, #13027, .T. ) ;
#191329=ORIENTED_EDGE ( 'NONE', *, *, #178844, .T. ) ;
#191594=ADVANCED_FACE ( 'NONE', ( #20720 ), #37724, .F. ) ;
#191846=B_SPLINE_CURVE_WITH_KNOTS ( 'NONE', 3,
 ( #69017, #148541, #169421, #84662, #89825, #45584, #70311, #228078, #226779, #49431 ),
 .UNSPECIFIED., .F., .F.,
 ( 4, 3, 3, 4 ),
 ( -2.000561356215401283E-06, 0.000000000000000000, 1.787822682428326401E-05, 4.206475347089222807E-05 ),
 .UNSPECIFIED. ) ;
#191921=DIRECTION ( 'NONE',  ( 0.000000000000000000, -0.9126074666063770380, -0.4088369013363281068 ) ) ;
#191958=ORIENTED_EDGE ( 'NONE', *, *, #130729, .F. ) ;
#192101=CARTESIAN_POINT ( 'NONE',  ( -16.90138253750126296, 51.49252402576821197, -232.0030672891792847 ) ) ;
#192241=( LENGTH_UNIT ( ) NAMED_UNIT ( * ) SI_UNIT ( .MILLI., .METRE. ) );
#192471=CARTESIAN_POINT ( 'NONE',  ( -16.84981964351488770, 51.43181437145960899, -232.0660758826369943 ) ) ;
#192498=DIRECTION ( 'NONE',  ( 1.652117596168391897E-15, -0.4088369013363281068, 0.9126074666063770380 ) ) ;
#192521=( BOUNDED_CURVE ( )  B_SPLINE_CURVE ( 3, ( #180359, #142492, #120418, #102071 ),
 .UNSPECIFIED., .F., .F. ) 
 B_SPLINE_CURVE_WITH_KNOTS ( ( 4, 4 ),
 ( 2.589852378279006384, 2.850972632318390154 ),
 .UNSPECIFIED. ) 
 CURVE ( )  GEOMETRIC_REPRESENTATION_ITEM ( )  RATIONAL_B_SPLINE_CURVE ( ( 1.000000000000000000, 0.9943260843901262636, 0.9943260843901262636, 1.000000000000000000 ) ) 
 REPRESENTATION_ITEM ( '' )  );
#192581=ORIENTED_EDGE ( 'NONE', *, *, #240226, .T. ) ;
#192852=ADVANCED_FACE ( 'NONE', ( #158698 ), #94832, .F. ) ;
#192871=B_SPLINE_CURVE_WITH_KNOTS ( 'NONE', 3,
 ( #114592, #98832, #177160, #194149, #18048, #16793, #15514, #96286, #95017, #158873, #218805, #234527, #97557 ),
 .UNSPECIFIED., .F., .F.,
 ( 4, 3, 3, 3, 4 ),
 ( 1.084445006577768341E-16, 1.946463881814435723E-05, 3.922356109944349927E-05, 4.215060953239166332E-05, 4.415117091093087289E-05 ),
 .UNSPECIFIED. ) ;
#193173=EDGE_LOOP ( 'NONE', ( #251174, #160504, #78209, #88911, #99986, #220863 ) ) ;
#193340=VECTOR ( 'NONE', #5924, 1000.000000000000114 ) ;
#193356=ADVANCED_FACE ( 'NONE', ( #181774 ), #223446, .F. ) ;
#193370=AXIS2_PLACEMENT_3D ( 'NONE', #62698, #224328, #136093 ) ;
#193754=CARTESIAN_POINT ( 'NONE',  ( -16.80891096016315700, 51.63498214198624225, -231.9392478082567948 ) ) ;
#194077=CARTESIAN_POINT ( 'NONE',  ( -13.77178122865953824, 46.49228253827788393, -234.7843890162627645 ) ) ;
#194149=CARTESIAN_POINT ( 'NONE',  ( -16.79814274880124358, 44.13799952519313763, -235.2986007742642300 ) ) ;
#194239=CARTESIAN_POINT ( 'NONE',  ( -16.93433913041102912, 51.67388201422455296, -231.8604821533804738 ) ) ;
#194500=PLANE ( 'NONE',  #116415 ) ;
#194605=DIRECTION ( 'NONE',  ( -1.000000000000000000, -6.754466386607082172E-16, 1.507734853975053202E-15 ) ) ;
#194708=ORIENTED_EDGE ( 'NONE', *, *, #242589, .F. ) ;
#194730=EDGE_LOOP ( 'NONE', ( #151744, #125259, #223542, #155677 ) ) ;
#194879=DIRECTION ( 'NONE',  ( -1.000000000000000000, 0.000000000000000000, 0.000000000000000000 ) ) ;
#194949=CARTESIAN_POINT ( 'NONE',  ( 12.25000000000000178, 47.91396133265956792, -234.2636761031308197 ) ) ;
#195128=VECTOR ( 'NONE', #108365, 1000.000000000000000 ) ;
#195253=CARTESIAN_POINT ( 'NONE',  ( 20.73486653747088582, 42.13647595316533057, -239.1530172309881550 ) ) ;
#195364=CARTESIAN_POINT ( 'NONE',  ( -14.87779219673428521, 46.70395665056642542, -234.7173882531051277 ) ) ;
#195405=VECTOR ( 'NONE', #2352, 1000.000000000000000 ) ;
#195412=PLANE ( 'NONE',  #11685 ) ;
#195643=LINE ( 'NONE', #215180, #203503 ) ;
#195883=AXIS2_PLACEMENT_3D ( 'NONE', #7625, #224086, #203250 ) ;
#196193=ORIENTED_EDGE ( 'NONE', *, *, #132070, .F. ) ;
#196309=CARTESIAN_POINT ( 'NONE',  ( -16.96982749440682170, 51.18557661132589232, -232.1405759491296976 ) ) ;
#196384=LINE ( 'NONE', #17735, #81288 ) ;
#196489=ORIENTED_EDGE ( 'NONE', *, *, #240035, .F. ) ;
#196500=AXIS2_PLACEMENT_3D ( 'NONE', #83601, #240157, #182759 ) ;
#196548=ADVANCED_FACE ( 'NONE', ( #203971 ), #127012, .F. ) ;
#196594=DIRECTION ( 'NONE',  ( 0.5932847527679310229, 0.3291107096594082515, -0.7346423231209699978 ) ) ;
#196611=CARTESIAN_POINT ( 'NONE',  ( -12.84409460144754078, 46.89406695649162060, -234.6540829047535510 ) ) ;
#196643=CARTESIAN_POINT ( 'NONE',  ( -15.75000000000000355, 48.12247445990688988, -234.1702647910923361 ) ) ;
#196762=CARTESIAN_POINT ( 'NONE',  ( -16.93262454970419384, 51.66793538483853609, -231.8674831426984042 ) ) ;
#196782=CARTESIAN_POINT ( 'NONE',  ( -18.34374000495059676, 54.09900352584866567, -229.1663746252470446 ) ) ;
#196871=EDGE_CURVE ( 'NONE', #230513, #32681, #109808, .T. ) ;
#197061=EDGE_LOOP ( 'NONE', ( #191329, #81756, #161120, #231573 ) ) ;
#197140=EDGE_CURVE ( 'NONE', #233724, #159477, #221691, .T. ) ;
#197188=DIRECTION ( 'NONE',  ( -1.073024830501117923E-15, -0.9126074666063771490, -0.4088369013363281623 ) ) ;
#197268=VECTOR ( 'NONE', #165135, 1000.000000000000114 ) ;
#197380=DIRECTION ( 'NONE',  ( -1.000000000000000000, 0.000000000000000000, 0.000000000000000000 ) ) ;
#197565=CARTESIAN_POINT ( 'NONE',  ( 14.88075390448864432, 49.48471825922439393, -233.4704840993163941 ) ) ;
#197593=CARTESIAN_POINT ( 'NONE',  ( -16.80621392010915827, 51.58591888298440864, -231.9697716580949702 ) ) ;
#197886=( BOUNDED_CURVE ( )  B_SPLINE_CURVE ( 3, ( #45904, #108447, #111011, #8073 ),
 .UNSPECIFIED., .F., .F. ) 
 B_SPLINE_CURVE_WITH_KNOTS ( ( 4, 4 ),
 ( 0.3000847527772382839, 0.5497968875596824789 ),
 .UNSPECIFIED. ) 
 CURVE ( )  GEOMETRIC_REPRESENTATION_ITEM ( )  RATIONAL_B_SPLINE_CURVE ( ( 1.000000000000000000, 0.9948104011409419911, 0.9948104011409419911, 1.000000000000000000 ) ) 
 REPRESENTATION_ITEM ( '' )  );
#197988=ORIENTED_EDGE ( 'NONE', *, *, #226132, .F. ) ;
#198016=EDGE_CURVE ( 'NONE', #201957, #240784, #182891, .T. ) ;
#198078=VECTOR ( 'NONE', #121325, 1000.000000000000114 ) ;
#198266=FACE_OUTER_BOUND ( 'NONE', #215297, .T. ) ;
#198280=CARTESIAN_POINT ( 'NONE',  ( -16.94107738177415712, 44.01795756907898749, -235.2811900454759382 ) ) ;
#198564=DIRECTION ( 'NONE',  ( 0.000000000000000000, 0.9126074666063660468, 0.4088369013363524762 ) ) ;
#198628=DIRECTION ( 'NONE',  ( -0.000000000000000000, 0.9126074666063770380, 0.4088369013363281068 ) ) ;
#198665=LINE ( 'NONE', #99535, #67877 ) ;
#198694=CARTESIAN_POINT ( 'NONE',  ( 20.27550659511088682, 41.33268472976309482, -237.3587910501520071 ) ) ;
#198777=CARTESIAN_POINT ( 'NONE',  ( -20.65000000000000568, 52.72272256579932304, -234.4105091754867942 ) ) ;
#198812=VECTOR ( 'NONE', #220407, 1000.000000000000114 ) ;
#198853=CARTESIAN_POINT ( 'NONE',  ( 12.30626653967341433, 48.53477651487869338, -233.9781183031097669 ) ) ;
#198904=CARTESIAN_POINT ( 'NONE',  ( -17.11825945287481687, 51.57797924205760864, -231.8552082689889460 ) ) ;
#198992=LINE ( 'NONE', #137716, #250045 ) ;
#199034=CARTESIAN_POINT ( 'NONE',  ( -16.88560720703333473, 44.13352770193326080, -235.2991880424075646 ) ) ;
#199772=CARTESIAN_POINT ( 'NONE',  ( 12.25000000000000000, 47.91805600923871822, -233.7139610577891631 ) ) ;
#199987=LINE ( 'NONE', #467, #115773 ) ;
#200151=CARTESIAN_POINT ( 'NONE',  ( 15.31784899511110076, 49.15934945732309558, -233.6546618023460553 ) ) ;
#200505=CARTESIAN_POINT ( 'NONE',  ( -15.15564720441980207, 49.30157392506337288, -233.5755204583867055 ) ) ;
#200667=CARTESIAN_POINT ( 'NONE',  ( -20.65000000000000568, 42.13647595316535188, -239.1530172309881834 ) ) ;
#200839=LINE ( 'NONE', #118746, #198812 ) ;
#201143=CARTESIAN_POINT ( 'NONE',  ( -21.64999999999999858, 41.27791846035906786, -237.2365415511148115 ) ) ;
#201420=CARTESIAN_POINT ( 'NONE',  ( 15.51872946208854920, 48.91191486804444111, -233.7874788057928868 ) ) ;
#201593=CARTESIAN_POINT ( 'NONE',  ( -16.87242674293850797, 44.13448673903910446, -235.2993773395560311 ) ) ;
#201778=CARTESIAN_POINT ( 'NONE',  ( -14.56336952470180179, 49.59862664907820573, -233.4030665626792711 ) ) ;
#201957=VERTEX_POINT ( 'NONE', #61098 ) ;
#202045=DIRECTION ( 'NONE',  ( -1.000000000000000000, 0.000000000000000000, 0.000000000000000000 ) ) ;
#202210=VECTOR ( 'NONE', #158773, 1000.000000000000000 ) ;
#202376=CARTESIAN_POINT ( 'NONE',  ( -16.97683809663752186, 44.82209472663103611, -234.9913374327310578 ) ) ;
#202618=DIRECTION ( 'NONE',  ( 1.000000000000000000, -9.792504721693619684E-16, -4.386921467590155985E-16 ) ) ;
#202752=LINE ( 'NONE', #142760, #185198 ) ;
#202794=ORIENTED_EDGE ( 'NONE', *, *, #85710, .T. ) ;
#202918=VERTEX_POINT ( 'NONE', #38075 ) ;
#202994=B_SPLINE_CURVE_WITH_KNOTS ( 'NONE', 3,
 ( #111574, #170307, #249796, #230228, #47723, #188535, #127281, #150698, #191134, #28216 ),
 .UNSPECIFIED., .F., .F.,
 ( 4, 3, 3, 4 ),
 ( 7.632826238673810152E-06, 4.756916949875324721E-05, 9.484459048150249510E-05, 0.0001435500935099965052 ),
 .UNSPECIFIED. ) ;
#203111=CARTESIAN_POINT ( 'NONE',  ( -16.89155683852559164, 44.70802594024834775, -235.0424388436548213 ) ) ;
#203127=CARTESIAN_POINT ( 'NONE',  ( -16.80100426158790938, 44.16834856606528348, -235.2917130533355135 ) ) ;
#203213=ORIENTED_EDGE ( 'NONE', *, *, #185958, .F. ) ;
#203224=DIRECTION ( 'NONE',  ( -1.000000000000000000, -0.000000000000000000, 0.000000000000000000 ) ) ;
#203250=DIRECTION ( 'NONE',  ( -1.000000000000000000, 0.000000000000000000, 0.000000000000000000 ) ) ;
#203340=CARTESIAN_POINT ( 'NONE',  ( -16.89797118371607354, 51.68774209830978350, -231.8867050212883498 ) ) ;
#203344=DIRECTION ( 'NONE',  ( 1.000000000000000000, 0.000000000000000000, 0.000000000000000000 ) ) ;
#203460=VECTOR ( 'NONE', #181236, 1000.000000000000114 ) ;
#203494=DIRECTION ( 'NONE',  ( 0.000000000000000000, 0.9126074666063660468, 0.4088369013363524762 ) ) ;
#203503=VECTOR ( 'NONE', #134340, 1000.000000000000000 ) ;
#203737=EDGE_CURVE ( 'NONE', #246882, #172022, #22714, .T. ) ;
#203881=DIRECTION ( 'NONE',  ( 1.186688945009010077E-16, 0.4088369013363281068, -0.9126074666063770380 ) ) ;
#203921=CARTESIAN_POINT ( 'NONE',  ( -23.25000000000000355, 45.89348038176515843, -239.2231437130149061 ) ) ;
#203932=APPLICATION_CONTEXT ( 'automotive_design' ) ;
#203943=VECTOR ( 'NONE', #96565, 1000.000000000000114 ) ;
#203971=FACE_OUTER_BOUND ( 'NONE', #59981, .T. ) ;
#204021=CARTESIAN_POINT ( 'NONE',  ( 21.13736287352038445, 44.91364453899298326, -237.0359499855415777 ) ) ;
#204321=AXIS2_PLACEMENT_3D ( 'NONE', #162212, #164758, #68227 ) ;
#204415=CARTESIAN_POINT ( 'NONE',  ( -16.92132318717937522, 44.10372977203042666, -235.2955471704553929 ) ) ;
#204680=ORIENTED_EDGE ( 'NONE', *, *, #13518, .F. ) ;
#204848=ADVANCED_FACE ( 'NONE', ( #236968 ), #54469, .F. ) ;
#204898=VERTEX_POINT ( 'NONE', #175735 ) ;
#205259=CARTESIAN_POINT ( 'NONE',  ( -16.94107738177415357, 44.01795756907897328, -235.2811900454759666 ) ) ;
#205553=FACE_OUTER_BOUND ( 'NONE', #147386, .T. ) ;
#205561=CARTESIAN_POINT ( 'NONE',  ( -16.91776028072577631, 51.63622145944459163, -231.9240089757377916 ) ) ;
#205641=ORIENTED_EDGE ( 'NONE', *, *, #217221, .F. ) ;
#205650=CARTESIAN_POINT ( 'NONE',  ( -18.37013991200266005, 54.12739742602126114, -229.1245229108895956 ) ) ;
#205824=DIRECTION ( 'NONE',  ( -0.000000000000000000, -0.9126074666063770380, -0.4088369013363281068 ) ) ;
#205898=DIRECTION ( 'NONE',  ( -0.7071067811865487940, -0.2890913453342125461, 0.6453109281988438362 ) ) ;
#206549=DIRECTION ( 'NONE',  ( 0.000000000000000000, 0.9126074666063769270, 0.4088369013363280513 ) ) ;
#206909=CARTESIAN_POINT ( 'NONE',  ( -17.11825945287482753, 44.09459801588531036, -235.2076708599468020 ) ) ;
#206967=CARTESIAN_POINT ( 'NONE',  ( -16.79270642812330294, 44.14711678134324302, -235.2978346781722223 ) ) ;
#207018=ORIENTED_EDGE ( 'NONE', *, *, #234562, .F. ) ;
#207048=CARTESIAN_POINT ( 'NONE',  ( -33.72168855820452649, 40.40989152675300033, -235.2989281452919954 ) ) ;
#207205=LINE ( 'NONE', #65106, #117265 ) ;
#207273=CARTESIAN_POINT ( 'NONE',  ( -16.81453563122430950, 51.56697356313223679, -231.9816583874184346 ) ) ;
#207447=VECTOR ( 'NONE', #227835, 999.9999999999998863 ) ;
#207601=LINE ( 'NONE', #124208, #36692 ) ;
#207743=ORIENTED_EDGE ( 'NONE', *, *, #91028, .F. ) ;
#207946=VECTOR ( 'NONE', #32285, 1000.000000000000000 ) ;
#208017=ORIENTED_EDGE ( 'NONE', *, *, #242589, .T. ) ;
#208252=EDGE_CURVE ( 'NONE', #245204, #225390, #134417, .T. ) ;
#208266=CARTESIAN_POINT ( 'NONE',  ( -16.77431908686106965, 44.15011970405063835, -235.2969698559747656 ) ) ;
#208355=ORIENTED_EDGE ( 'NONE', *, *, #98572, .F. ) ;
#208446=CARTESIAN_POINT ( 'NONE',  ( -16.87368910959167678, 44.09664347368151738, -235.3039772434659085 ) ) ;
#208503=LINE ( 'NONE', #92372, #161973 ) ;
#208772=DIRECTION ( 'NONE',  ( 0.000000000000000000, 0.4088369013363783999, -0.9126074666063545004 ) ) ;
#208870=ORIENTED_EDGE ( 'NONE', *, *, #254699, .T. ) ;
#208918=EDGE_CURVE ( 'NONE', #202918, #108079, #156035, .T. ) ;
#209076=CARTESIAN_POINT ( 'NONE',  ( -16.97048361161166596, 51.17066711795111900, -232.1472552184704341 ) ) ;
#209408=DIRECTION ( 'NONE',  ( -1.000000000000000000, 0.000000000000000000, 0.000000000000000000 ) ) ;
#209424=CARTESIAN_POINT ( 'NONE',  ( -16.90128866880175806, 51.62887945800996192, -231.9378224694952166 ) ) ;
#209534=CARTESIAN_POINT ( 'NONE',  ( -16.87401514999234564, 44.19934780856234369, -235.2703203795249749 ) ) ;
#209825=VECTOR ( 'NONE', #251818, 1000.000000000000114 ) ;
#210040=DIRECTION ( 'NONE',  ( 1.000000000000000000, 0.000000000000000000, 0.000000000000000000 ) ) ;
#210192=VERTEX_POINT ( 'NONE', #229227 ) ;
#210215=CARTESIAN_POINT ( 'NONE',  ( 18.39999999999999503, 56.47972699439914379, -234.4806356575134885 ) ) ;
#210289=ORIENTED_EDGE ( 'NONE', *, *, #216011, .F. ) ;
#210371=CARTESIAN_POINT ( 'NONE',  ( -16.86133551771148475, 51.57445858725908749, -231.9663616150992027 ) ) ;
#210443=AXIS2_PLACEMENT_3D ( 'NONE', #184143, #83727, #71605 ) ;
#210551=VERTEX_POINT ( 'NONE', #5987 ) ;
#210818=CARTESIAN_POINT ( 'NONE',  ( -16.80621392010893445, 44.17480150332616518, -235.2898609361353124 ) ) ;
#210917=ORIENTED_EDGE ( 'NONE', *, *, #8340, .F. ) ;
#211017=DIRECTION ( 'NONE',  ( -0.000000000000000000, 0.9126074666063770380, 0.4088369013363281068 ) ) ;
#211035=CARTESIAN_POINT ( 'NONE',  ( -20.65000000000000568, 42.13647595316535188, -239.1530172309881834 ) ) ;
#211180=B_SPLINE_CURVE_WITH_KNOTS ( 'NONE', 3,
 ( #146988, #44061, #244811, #203127, #27095, #145707, #227822, #187432, #109148, #188699, #225234, #148298, #46599, #126144 ),
 .UNSPECIFIED., .F., .F.,
 ( 4, 2, 2, 2, 2, 2, 4 ),
 ( 0.000000000000000000, 2.389617747641528420E-05, 4.779235495283056841E-05, 9.558470990567925654E-05, 0.0001911694198113798448, 0.0003823388396228040876, 0.0007646776792456565306 ),
 .UNSPECIFIED. ) ;
#211205=CARTESIAN_POINT ( 'NONE',  ( -16.93344882324368683, 51.65733344460321064, -231.8781845289940691 ) ) ;
#211293=VERTEX_POINT ( 'NONE', #246256 ) ;
#211569=CARTESIAN_POINT ( 'NONE',  ( -12.25000000000000178, 47.91805600923872532, -233.7139610577891631 ) ) ;
#211686=DIRECTION ( 'NONE',  ( 1.186688945009010077E-16, 0.4088369013363280513, -0.9126074666063769270 ) ) ;
#211698=VERTEX_POINT ( 'NONE', #253621 ) ;
#211912=PLANE ( 'NONE',  #113676 ) ;
#211938=CARTESIAN_POINT ( 'NONE',  ( 13.22261339317536866, 46.65242889160096951, -234.7339858363277187 ) ) ;
#211959=ORIENTED_EDGE ( 'NONE', *, *, #70550, .T. ) ;
#212010=DIRECTION ( 'NONE',  ( -0.7071067811865457964, -0.2890913453342137673, 0.6453109281988465007 ) ) ;
#212073=CARTESIAN_POINT ( 'NONE',  ( -33.72168855820452649, 54.09900352584866567, -229.1663746252470446 ) ) ;
#212118=ORIENTED_EDGE ( 'NONE', *, *, #135415, .F. ) ;
#212162=EDGE_CURVE ( 'NONE', #125918, #114829, #186511, .T. ) ;
#212441=EDGE_LOOP ( 'NONE', ( #57181, #229820, #204680, #197988 ) ) ;
#212504=AXIS2_PLACEMENT_3D ( 'NONE', #47994, #127543, #247485 ) ;
#212622=VERTEX_POINT ( 'NONE', #206909 ) ;
#212682=VERTEX_POINT ( 'NONE', #71273 ) ;
#212758=ORIENTED_EDGE ( 'NONE', *, *, #181331, .F. ) ;
#212953=CYLINDRICAL_SURFACE ( 'NONE', #79552, 1.749999999999998002 ) ;
#213181=ORIENTED_EDGE ( 'NONE', *, *, #208252, .F. ) ;
#213226=EDGE_CURVE ( 'NONE', #211698, #2625, #207601, .T. ) ;
#213326=EDGE_CURVE ( 'NONE', #120740, #115352, #87614, .T. ) ;
#213606=CARTESIAN_POINT ( 'NONE',  ( -15.75000000000000355, 48.12247445990688988, -234.1702647910923361 ) ) ;
#213609=DIRECTION ( 'NONE',  ( 0.5932847527679310229, 0.3291107096594076964, -0.7346423231209702198 ) ) ;
#213668=AXIS2_PLACEMENT_3D ( 'NONE', #160464, #99149, #79586 ) ;
#213760=VERTEX_POINT ( 'NONE', #158552 ) ;
#214002=VECTOR ( 'NONE', #211017, 1000.000000000000114 ) ;
#214397=EDGE_LOOP ( 'NONE', ( #15523, #94584, #41459, #66688 ) ) ;
#215176=ORIENTED_EDGE ( 'NONE', *, *, #40950, .F. ) ;
#215180=CARTESIAN_POINT ( 'NONE',  ( -23.25000000000000355, 40.29670989715187090, -235.0462836312595130 ) ) ;
#215297=EDGE_LOOP ( 'NONE', ( #256433, #160780, #8470, #114594, #202794, #57009, #126762, #256962, #168919, #9254, #71985, #249058, #233191, #41562, #246549, #68177, #218828, #190659 ) ) ;
#215503=EDGE_CURVE ( 'NONE', #47203, #68795, #198992, .T. ) ;
#215610=ORIENTED_EDGE ( 'NONE', *, *, #84653, .T. ) ;
#215757=CARTESIAN_POINT ( 'NONE',  ( 15.74999999999999645, 48.12247445990688988, -234.1702647910923361 ) ) ;
#216011=EDGE_CURVE ( 'NONE', #163693, #56126, #192871, .T. ) ;
#216169=CARTESIAN_POINT ( 'NONE',  ( -13.12432614554022514, 46.70278183066206878, -234.7177704364561350 ) ) ;
#216175=DIRECTION ( 'NONE',  ( 1.000000000000000000, 0.000000000000000000, 0.000000000000000000 ) ) ;
#216515=CYLINDRICAL_SURFACE ( 'NONE', #118466, 0.09999999999999939493 ) ;
#216670=ORIENTED_EDGE ( 'NONE', *, *, #40950, .T. ) ;
#216783=DIRECTION ( 'NONE',  ( 1.186688945009010077E-16, 0.4088369013363280513, -0.9126074666063769270 ) ) ;
#216806=CARTESIAN_POINT ( 'NONE',  ( -20.65000000000000568, 52.72272256579932304, -234.4105091754867942 ) ) ;
#217086=EDGE_CURVE ( 'NONE', #238714, #167295, #98532, .T. ) ;
#217111=CARTESIAN_POINT ( 'NONE',  ( 15.69410316191959609, 48.53345590596379111, -233.9787581418636364 ) ) ;
#217138=FACE_OUTER_BOUND ( 'NONE', #10265, .T. ) ;
#217221=EDGE_CURVE ( 'NONE', #114829, #157279, #231714, .T. ) ;
#217444=PLANE ( 'NONE',  #242695 ) ;
#217691=SHAPE_DEFINITION_REPRESENTATION ( #242846, #141939 ) ;
#217720=FACE_OUTER_BOUND ( 'NONE', #142184, .T. ) ;
#217772=CARTESIAN_POINT ( 'NONE',  ( -18.35663730107557257, 40.40958672937900076, -235.2982477752999273 ) ) ;
#217813=FACE_BOUND ( 'NONE', #117210, .T. ) ;
#217866=CARTESIAN_POINT ( 'NONE',  ( -16.87683809663752399, 42.27269979661959098, -221.1123729563994402 ) ) ;
#218200=ORIENTED_EDGE ( 'NONE', *, *, #232612, .F. ) ;
#218237=ADVANCED_FACE ( 'NONE', ( #34207 ), #28451, .T. ) ;
#218435=DIRECTION ( 'NONE',  ( 0.000000000000000000, -0.4088369013363281068, 0.9126074666063770380 ) ) ;
#218480=CARTESIAN_POINT ( 'NONE',  ( -17.22361732159832215, 42.80650589791834193, -235.4613000926810855 ) ) ;
#218572=CARTESIAN_POINT ( 'NONE',  ( -16.88815647973234135, 44.13260157173010612, -235.2993095192094870 ) ) ;
#218764=CARTESIAN_POINT ( 'NONE',  ( -12.33960340485503338, 48.63331072832804836, -233.9296379114950355 ) ) ;
#218805=CARTESIAN_POINT ( 'NONE',  ( -16.77779411503079032, 44.14899187519263535, -235.2971511010943004 ) ) ;
#218828=ORIENTED_EDGE ( 'NONE', *, *, #35605, .F. ) ;
#218854=ORIENTED_EDGE ( 'NONE', *, *, #135415, .T. ) ;
#219030=CARTESIAN_POINT ( 'NONE',  ( -16.86445178670615874, 51.65108416207809938, -231.9186532702945556 ) ) ;
#219040=ORIENTED_EDGE ( 'NONE', *, *, #137624, .T. ) ;
#219437=DIRECTION ( 'NONE',  ( 1.186688945009010077E-16, 0.4088369013363281623, -0.9126074666063771490 ) ) ;
#219465=LINE ( 'NONE', #160822, #143926 ) ;
#219480=CARTESIAN_POINT ( 'NONE',  ( -18.40000000000000213, 53.37686160793744961, -235.8706811220569932 ) ) ;
#219694=CARTESIAN_POINT ( 'NONE',  ( 13.12229106158772751, 49.47508301341328263, -233.4759538034894319 ) ) ;
#219827=CARTESIAN_POINT ( 'NONE',  ( -16.77683809663752257, 42.27269979661959098, -221.1123729563994402 ) ) ;
#219848=ORIENTED_EDGE ( 'NONE', *, *, #187158, .T. ) ;
#219915=ORIENTED_EDGE ( 'NONE', *, *, #190321, .F. ) ;
#220118=ORIENTED_EDGE ( 'NONE', *, *, #26354, .T. ) ;
#220314=LINE ( 'NONE', #16986, #136123 ) ;
#220344=CARTESIAN_POINT ( 'NONE',  ( -16.85718274719440046, 51.68725577354657474, -231.8871841270915013 ) ) ;
#220405=FACE_OUTER_BOUND ( 'NONE', #238658, .T. ) ;
#220407=DIRECTION ( 'NONE',  ( -0.000000000000000000, 0.9126074666063770380, 0.4088369013363281068 ) ) ;
#220467=FACE_OUTER_BOUND ( 'NONE', #87959, .T. ) ;
#220656=EDGE_CURVE ( 'NONE', #211293, #68795, #220314, .T. ) ;
#220822=( NAMED_UNIT ( * ) PLANE_ANGLE_UNIT ( ) SI_UNIT ( $, .RADIAN. ) );
#220863=ORIENTED_EDGE ( 'NONE', *, *, #180891, .T. ) ;
#220883=CARTESIAN_POINT ( 'NONE',  ( 18.39999999999999503, 53.37686160793744961, -235.8706811220569932 ) ) ;
#221148=CARTESIAN_POINT ( 'NONE',  ( -16.95709691156226384, 44.14466031266160684, -235.2948197039139870 ) ) ;
#221230=ORIENTED_EDGE ( 'NONE', *, *, #155188, .T. ) ;
#221327=CARTESIAN_POINT ( 'NONE',  ( -13.77083647240106679, 49.67554723225254776, -233.3568105763834524 ) ) ;
#221393=ORIENTED_EDGE ( 'NONE', *, *, #174157, .F. ) ;
#221438=DIRECTION ( 'NONE',  ( -1.000000000000000000, 0.000000000000000000, 0.000000000000000000 ) ) ;
#221542=CIRCLE ( 'NONE', #109118, 14.30833333333333535 ) ;
#221595=CARTESIAN_POINT ( 'NONE',  ( -15.55912972643740488, 52.21540900819563547, -233.2780816987436765 ) ) ;
#221691=B_SPLINE_CURVE_WITH_KNOTS ( 'NONE', 3,
 ( #73186, #225782, #48447, #217772, #136969, #254333, #35348 ),
 .UNSPECIFIED., .F., .F.,
 ( 4, 3, 4 ),
 ( 0.000000000000000000, 4.520325912680621513E-05, 5.794988040901376952E-05 ),
 .UNSPECIFIED. ) ;
#221735=FACE_OUTER_BOUND ( 'NONE', #75526, .T. ) ;
#221756=DIRECTION ( 'NONE',  ( 0.000000000000000000, -0.4088369013363281068, 0.9126074666063770380 ) ) ;
#222079=( NAMED_UNIT ( * ) SI_UNIT ( $, .STERADIAN. ) SOLID_ANGLE_UNIT ( ) );
#222262=CARTESIAN_POINT ( 'NONE',  ( -16.88005004766534967, 51.61912858099893242, -231.9462398806007286 ) ) ;
#222336=ORIENTED_EDGE ( 'NONE', *, *, #109984, .F. ) ;
#222550=ORIENTED_EDGE ( 'NONE', *, *, #15821, .T. ) ;
#222606=( GEOMETRIC_REPRESENTATION_CONTEXT ( 3 ) GLOBAL_UNCERTAINTY_ASSIGNED_CONTEXT ( ( #133757 ) ) GLOBAL_UNIT_ASSIGNED_CONTEXT ( ( #103423, #220822, #162163 ) ) REPRESENTATION_CONTEXT ( 'NONE', 'WORKASPACE' ) );
#222772=ORIENTED_EDGE ( 'NONE', *, *, #213226, .T. ) ;
#222888=LINE ( 'NONE', #165510, #179817 ) ;
#222924=EDGE_LOOP ( 'NONE', ( #144098, #238991, #210289, #175722 ) ) ;
#223046=FACE_OUTER_BOUND ( 'NONE', #111629, .T. ) ;
#223085=CARTESIAN_POINT ( 'NONE',  ( 20.73486653747088226, 45.23934133962701765, -237.7629717664446503 ) ) ;
#223158=EDGE_CURVE ( 'NONE', #77934, #211293, #230865, .T. ) ;
#223224=DIRECTION ( 'NONE',  ( 1.000000000000000000, 0.000000000000000000, 0.000000000000000000 ) ) ;
#223299=EDGE_CURVE ( 'NONE', #172948, #14805, #155587, .T. ) ;
#223446=PLANE ( 'NONE',  #50055 ) ;
#223449=PLANE ( 'NONE',  #170539 ) ;
#223542=ORIENTED_EDGE ( 'NONE', *, *, #74252, .T. ) ;
#223809=EDGE_CURVE ( 'NONE', #245204, #7237, #192521, .T. ) ;
#224086=DIRECTION ( 'NONE',  ( -1.073024830501117923E-15, 0.9126074666063771490, 0.4088369013363281623 ) ) ;
#224182=ADVANCED_FACE ( 'NONE', ( #54938 ), #194500, .T. ) ;
#224328=DIRECTION ( 'NONE',  ( 1.186688945009009831E-16, 0.4088369013363281068, -0.9126074666063770380 ) ) ;
#224586=CARTESIAN_POINT ( 'NONE',  ( -18.39999999999999858, 40.47920047438133651, -235.2678785906695396 ) ) ;
#224743=ORIENTED_EDGE ( 'NONE', *, *, #113241, .T. ) ;
#224823=AXIS2_PLACEMENT_3D ( 'NONE', #7707, #67662, #202045 ) ;
#225204=CARTESIAN_POINT ( 'NONE',  ( -17.80356949363931918, 53.39653902550993081, -230.1346155703532759 ) ) ;
#225217=CARTESIAN_POINT ( 'NONE',  ( -16.87683809663752399, 44.86297841676467613, -235.0825981793917379 ) ) ;
#225234=CARTESIAN_POINT ( 'NONE',  ( -16.85939591225058010, 44.43675737074195098, -235.2130249156476793 ) ) ;
#225366=CARTESIAN_POINT ( 'NONE',  ( -18.40000000000000213, 53.37686160793744961, -235.8706811220569932 ) ) ;
#225390=VERTEX_POINT ( 'NONE', #79683 ) ;
#225552=CARTESIAN_POINT ( 'NONE',  ( -18.40000000000000213, 45.89348038176515843, -239.2231437130149061 ) ) ;
#225782=CARTESIAN_POINT ( 'NONE',  ( -18.38639463286148867, 40.40701426736398361, -235.2925055146703528 ) ) ;
#225972=DIRECTION ( 'NONE',  ( 1.000000000000000000, 0.000000000000000000, -0.000000000000000000 ) ) ;
#226132=EDGE_CURVE ( 'NONE', #152864, #75024, #54390, .T. ) ;
#226268=CARTESIAN_POINT ( 'NONE',  ( -17.11825945287483108, 44.09459801588531036, -235.2076708599468020 ) ) ;
#226401=CARTESIAN_POINT ( 'NONE',  ( -16.89268316805465986, 51.62340874627276577, -231.9425458505251072 ) ) ;
#226611=ORIENTED_EDGE ( 'NONE', *, *, #28596, .F. ) ;
#226625=FACE_OUTER_BOUND ( 'NONE', #24846, .T. ) ;
#226740=AXIS2_PLACEMENT_3D ( 'NONE', #62397, #38998, #221438 ) ;
#226779=CARTESIAN_POINT ( 'NONE',  ( -16.80939487329394666, 51.61886293219204447, -231.9464690156492281 ) ) ;
#226785=VERTEX_POINT ( 'NONE', #23970 ) ;
#226809=CARTESIAN_POINT ( 'NONE',  ( -16.80100914604136975, 51.59158805982346507, -231.9661947804042370 ) ) ;
#226826=AXIS2_PLACEMENT_3D ( 'NONE', #73656, #35806, #194879 ) ;
#226830=LINE ( 'NONE', #48188, #257409 ) ;
#226859=EDGE_CURVE ( 'NONE', #228856, #245204, #77, .T. ) ;
#227135=DIRECTION ( 'NONE',  ( -1.000000000000000000, -0.000000000000000000, -0.000000000000000000 ) ) ;
#227211=EDGE_CURVE ( 'NONE', #212622, #210192, #137974, .T. ) ;
#227331=CARTESIAN_POINT ( 'NONE',  ( 18.39999999999999503, 53.98582189624753624, -228.9137301112145622 ) ) ;
#227333=DIRECTION ( 'NONE',  ( 0.000000000000000000, -0.4088369013363281068, 0.9126074666063770380 ) ) ;
#227458=CARTESIAN_POINT ( 'NONE',  ( 18.39999999999999503, 43.39957528361355799, -233.6562381667159798 ) ) ;
#227711=ORIENTED_EDGE ( 'NONE', *, *, #147414, .F. ) ;
#227792=CARTESIAN_POINT ( 'NONE',  ( -16.93255653858138388, 44.05329019094499898, -235.2826611615568595 ) ) ;
#227822=CARTESIAN_POINT ( 'NONE',  ( -16.81930730667009044, 44.21085617933544398, -235.2794117849574320 ) ) ;
#227835=DIRECTION ( 'NONE',  ( 0.7071067811865463515, -0.2890913453342142114, 0.6453109281988457235 ) ) ;
#227879=EDGE_LOOP ( 'NONE', ( #249195, #72483, #98356, #80394 ) ) ;
#227988=CARTESIAN_POINT ( 'NONE',  ( -16.87845715379269507, 44.10835929761906016, -235.3024714938296995 ) ) ;
#228078=CARTESIAN_POINT ( 'NONE',  ( -16.80117486205003630, 51.61795800203399409, -231.9472499653515740 ) ) ;
#228283=CARTESIAN_POINT ( 'NONE',  ( -18.35668295345803713, 54.09900352584866567, -229.1663746252470446 ) ) ;
#228319=CARTESIAN_POINT ( 'NONE',  ( -16.89268316805466341, 44.12952801035616801, -235.2997120924900969 ) ) ;
#228387=CARTESIAN_POINT ( 'NONE',  ( 21.72449340488910252, 43.99894805634765760, -234.9941606142489832 ) ) ;
#228464=CARTESIAN_POINT ( 'NONE',  ( 23.04999999999999716, 55.18266668263805030, -231.5853321237989633 ) ) ;
#228661=CARTESIAN_POINT ( 'NONE',  ( -16.84419801905645997, 51.60107635300602169, -231.9544371839865562 ) ) ;
#228714=CARTESIAN_POINT ( 'NONE',  ( -17.22767730082796689, 42.79277586624079532, -235.4629708983620446 ) ) ;
#228856=VERTEX_POINT ( 'NONE', #46311 ) ;
#228970=DIRECTION ( 'NONE',  ( 0.000000000000000000, 0.9126074666063770380, 0.4088369013363281068 ) ) ;
#229008=CARTESIAN_POINT ( 'NONE',  ( -16.94389599337535657, 51.64067334384618846, -231.8915550546001612 ) ) ;
#229171=CARTESIAN_POINT ( 'NONE',  ( -21.64999999999999858, 51.57797924205760864, -231.8552082689889460 ) ) ;
#229227=CARTESIAN_POINT ( 'NONE',  ( -18.40000000000000213, 43.57057518228153015, -234.0379448663882442 ) ) ;
#229279=CARTESIAN_POINT ( 'NONE',  ( -16.89268316805466341, 44.12952801035616801, -235.2997120924900969 ) ) ;
#229440=DIRECTION ( 'NONE',  ( 0.000000000000000000, 0.9126074666063770380, 0.4088369013363281068 ) ) ;
#229594=DIRECTION ( 'NONE',  ( 1.186688945009010077E-16, 0.4088369013363280513, -0.9126074666063769270 ) ) ;
#229700=CARTESIAN_POINT ( 'NONE',  ( 18.39999999999999503, 43.51275691321468031, -233.9088826807484622 ) ) ;
#229820=ORIENTED_EDGE ( 'NONE', *, *, #203737, .T. ) ;
#229885=( BOUNDED_SURFACE ( )  B_SPLINE_SURFACE ( 3, 2, ( 
 ( #244796, #123582, #225217 ),
 ( #57489, #203111, #103985 ),
 ( #255662, #183560, #46585 ),
 ( #4882, #126127, #28369 ),
 ( #88269, #49171, #11335 ),
 ( #107858, #187417, #90861 ),
 ( #209534, #8770, #132571 ),
 ( #71329, #149584, #210818 ),
 ( #89572, #150840, #206967 ),
 ( #68747, #249947, #208266 ) ),
 .UNSPECIFIED., .F., .F., .F. ) 
 B_SPLINE_SURFACE_WITH_KNOTS ( ( 4, 2, 2, 2, 4 ),
 ( 3, 3 ),
 ( 0.002161241639767788603, 0.002579950749617450703, 0.002789305304542281753, 0.002893982582004697712, 0.002998659859467113237 ),
 ( 0.000000000000000000, 1.000000000000000000 ),
 .UNSPECIFIED. ) 
 GEOMETRIC_REPRESENTATION_ITEM ( )  RATIONAL_B_SPLINE_SURFACE ( (
 ( 1.000000000000000000, 0.7071067811864479857, 1.000000000000000000),
 ( 1.000000000000000000, 0.7632447400663979753, 1.000000000000000000),
 ( 1.000000000000000000, 0.8158073005110251241, 1.000000000000000000),
 ( 1.000000000000000000, 0.8906973462395024743, 1.000000000000000000),
 ( 1.000000000000000000, 0.9149408947808339576, 1.000000000000000000),
 ( 1.000000000000000000, 0.9493368785271785182, 1.000000000000000000),
 ( 1.000000000000000000, 0.9605194247157303744, 1.000000000000000000),
 ( 1.000000000000000000, 0.9803630264780529568, 1.000000000000000000),
 ( 1.000000000000000000, 0.9900844824271433087, 1.000000000000000000),
 ( 1.000000000000000000, 0.9894588281429317345, 1.000000000000000000) ) ) 
 REPRESENTATION_ITEM ( '' )  SURFACE ( )  );
#230201=CARTESIAN_POINT ( 'NONE',  ( 14.22821877134045998, 46.49228253827787682, -234.7843890162627360 ) ) ;
#230228=CARTESIAN_POINT ( 'NONE',  ( -16.87304349924914604, 51.64971365025504468, -231.9197784714389741 ) ) ;
#230513=VERTEX_POINT ( 'NONE', #211569 ) ;
#230588=CARTESIAN_POINT ( 'NONE',  ( 22.88900146558018989, 52.12831263616270405, -233.0836648073824335 ) ) ;
#230865=LINE ( 'NONE', #90032, #99069 ) ;
#231242=ORIENTED_EDGE ( 'NONE', *, *, #123918, .T. ) ;
#231280=ORIENTED_EDGE ( 'NONE', *, *, #38873, .F. ) ;
#231573=ORIENTED_EDGE ( 'NONE', *, *, #112376, .T. ) ;
#231672=CARTESIAN_POINT ( 'NONE',  ( -16.94180778212363236, 44.07631700300555622, -235.2789292040941973 ) ) ;
#231714=LINE ( 'NONE', #167904, #151684 ) ;
#231903=CARTESIAN_POINT ( 'NONE',  ( 21.13736287352038445, 52.39702576516527444, -233.6834873945836932 ) ) ;
#232032=ORIENTED_EDGE ( 'NONE', *, *, #217086, .F. ) ;
#232254=EDGE_CURVE ( 'NONE', #204898, #202918, #87422, .T. ) ;
#232325=EDGE_CURVE ( 'NONE', #210192, #131621, #89991, .T. ) ;
#232497=VECTOR ( 'NONE', #35406, 1000.000000000000114 ) ;
#232516=CARTESIAN_POINT ( 'NONE',  ( -16.97683809663755028, 51.05165077286171282, -232.2005730747396512 ) ) ;
#232612=EDGE_CURVE ( 'NONE', #69236, #204898, #37243, .T. ) ;
#232746=ORIENTED_EDGE ( 'NONE', *, *, #93427, .T. ) ;
#232792=CARTESIAN_POINT ( 'NONE',  ( 12.47034474403012538, 47.30882569885141464, -234.5067857460874166 ) ) ;
#232906=CARTESIAN_POINT ( 'NONE',  ( -16.79270642812257108, 51.61029886228697450, -231.9544210554141728 ) ) ;
#232931=DIRECTION ( 'NONE',  ( 1.000000000000000000, 0.000000000000000000, 0.000000000000000000 ) ) ;
#232960=CARTESIAN_POINT ( 'NONE',  ( -16.94445028196808778, 44.07934375239701552, -235.2779890399608576 ) ) ;
#233191=ORIENTED_EDGE ( 'NONE', *, *, #109984, .T. ) ;
#233196=LINE ( 'NONE', #151069, #21339 ) ;
#233724=VERTEX_POINT ( 'NONE', #93588 ) ;
#233855=ORIENTED_EDGE ( 'NONE', *, *, #191303, .T. ) ;
#233917=SURFACE_STYLE_FILL_AREA ( #151841 ) ;
#233923=CIRCLE ( 'NONE', #196500, 14.30833333333333357 ) ;
#234223=VECTOR ( 'NONE', #78814, 1000.000000000000114 ) ;
#234292=ORIENTED_EDGE ( 'NONE', *, *, #66520, .F. ) ;
#234305=CARTESIAN_POINT ( 'NONE',  ( 15.74999999999999645, 47.91805600923871822, -233.7139610577891631 ) ) ;
#234527=CARTESIAN_POINT ( 'NONE',  ( -16.77732147278574715, 44.14945876519793444, -235.2970893357522755 ) ) ;
#234562=EDGE_CURVE ( 'NONE', #125918, #68814, #222888, .T. ) ;
#234621=EDGE_CURVE ( 'NONE', #68788, #126269, #207205, .T. ) ;
#234681=ADVANCED_FACE ( 'NONE', ( #68986 ), #46809, .F. ) ;
#234851=CARTESIAN_POINT ( 'NONE',  ( 18.39999999999998082, 40.40989152675300033, -235.2989281452919954 ) ) ;
#235330=CARTESIAN_POINT ( 'NONE',  ( 15.74999999999999645, 47.91126876242802979, -234.2648823414208152 ) ) ;
#235428=CARTESIAN_POINT ( 'NONE',  ( -16.89155683852526479, 51.04631869796540400, -232.2029617786061522 ) ) ;
#235451=CARTESIAN_POINT ( 'NONE',  ( -16.93388492042257809, 51.64923346972221196, -231.8906307491038206 ) ) ;
#235815=LINE ( 'NONE', #19348, #164379 ) ;
#236019=ORIENTED_EDGE ( 'NONE', *, *, #234621, .T. ) ;
#236081=EDGE_CURVE ( 'NONE', #115352, #233724, #187604, .T. ) ;
#236409=COLOUR_RGB ( '', 0.72549020, 0.75294118, 0.79215686) ;
#236431=ADVANCED_FACE ( 'NONE', ( #175520 ), #112573, .T. ) ;
#236449=EDGE_CURVE ( 'NONE', #213760, #251476, #2862, .T. ) ;
#236507=DIRECTION ( 'NONE',  ( -0.000000000000000000, 0.9126074666063769270, 0.4088369013363280513 ) ) ;
#236685=CARTESIAN_POINT ( 'NONE',  ( 14.22916352759893499, 49.67554723225254065, -233.3568105763834524 ) ) ;
#236711=CARTESIAN_POINT ( 'NONE',  ( -16.82542659449973499, 51.53883479335955542, -231.9993050559371284 ) ) ;
#236968=FACE_OUTER_BOUND ( 'NONE', #90600, .T. ) ;
#237045=ORIENTED_EDGE ( 'NONE', *, *, #223299, .F. ) ;
#237540=VERTEX_POINT ( 'NONE', #191281 ) ;
#237592=ORIENTED_EDGE ( 'NONE', *, *, #104355, .T. ) ;
#237973=CARTESIAN_POINT ( 'NONE',  ( 12.60873083341396317, 49.08063300121914807, -233.6976605013539654 ) ) ;
#237992=CARTESIAN_POINT ( 'NONE',  ( -16.88593481969334320, 51.62034258236364082, -231.9451924255289441 ) ) ;
#238143=CARTESIAN_POINT ( 'NONE',  ( -16.89268316805466341, 44.12952801035616801, -235.2997120924900969 ) ) ;
#238194=B_SPLINE_CURVE_WITH_KNOTS ( 'NONE', 3,
 ( #180947, #42711, #240918, #182235, #218764, #122257, #178405, #40178, #256571, #179671, #98797, #100088, #221327, #257857, #117124, #20606, #201778, #37599, #80521, #79247, #200505, #77977, #119699, #157573, #41454, #177119, #978, #57115, #62277, #196643 ),
 .UNSPECIFIED., .F., .F.,
 ( 4, 2, 2, 2, 2, 2, 2, 2, 2, 2, 2, 2, 2, 2, 4 ),
 ( 0.000000000000000000, 0.0003422764154113468963, 0.0006845528308226937926, 0.001026829246234040689, 0.001369105661645387585, 0.002053658492468048852, 0.002738211323290710986, 0.003080487738702042053, 0.003422764154113372686, 0.003765040569524704187, 0.004107316984936035253, 0.004449593400347366320, 0.004791869815758697387, 0.005134146231170028454, 0.005476422646581359521 ),
 .UNSPECIFIED. ) ;
#238268=FACE_OUTER_BOUND ( 'NONE', #73335, .T. ) ;
#238649=ORIENTED_EDGE ( 'NONE', *, *, #21489, .F. ) ;
#238658=EDGE_LOOP ( 'NONE', ( #135076, #188818, #185501, #45963 ) ) ;
#238714=VERTEX_POINT ( 'NONE', #228319 ) ;
#238991=ORIENTED_EDGE ( 'NONE', *, *, #97066, .F. ) ;
#239318=ORIENTED_EDGE ( 'NONE', *, *, #223158, .F. ) ;
#239338=DIRECTION ( 'NONE',  ( -0.000000000000000000, 0.9126074666063770380, 0.4088369013363281068 ) ) ;
#239357=CARTESIAN_POINT ( 'NONE',  ( -17.71734398241073905, 41.60308423793308918, -235.4556039006346850 ) ) ;
#239637=CARTESIAN_POINT ( 'NONE',  ( -18.39999999999999858, 40.47920047438133651, -235.2678785906695396 ) ) ;
#239869=EDGE_CURVE ( 'NONE', #107188, #210551, #53435, .T. ) ;
#239991=CARTESIAN_POINT ( 'NONE',  ( -16.89797118371642881, 44.04503171409839979, -235.3105451120472082 ) ) ;
#240011=ORIENTED_EDGE ( 'NONE', *, *, #19629, .F. ) ;
#240035=EDGE_CURVE ( 'NONE', #19773, #91807, #18286, .T. ) ;
#240113=EDGE_CURVE ( 'NONE', #74012, #211698, #241206, .T. ) ;
#240157=DIRECTION ( 'NONE',  ( 1.000000000000000000, 0.000000000000000000, 0.000000000000000000 ) ) ;
#240226=EDGE_CURVE ( 'NONE', #233724, #243788, #208503, .T. ) ;
#240287=PLANE ( 'NONE',  #125618 ) ;
#240356=FACE_OUTER_BOUND ( 'NONE', #184270, .T. ) ;
#240424=CIRCLE ( 'NONE', #161329, 0.9000000000000014655 ) ;
#240511=MECHANICAL_DESIGN_GEOMETRIC_PRESENTATION_REPRESENTATION('',(#15689),#74130);
#240540=DIRECTION ( 'NONE',  ( 1.000000000000000000, 0.000000000000000000, -0.000000000000000000 ) ) ;
#240559=CARTESIAN_POINT ( 'NONE',  ( 15.39170923737819763, 49.08016403251641435, -233.6979168753148883 ) ) ;
#240616=ORIENTED_EDGE ( 'NONE', *, *, #213226, .F. ) ;
#240784=VERTEX_POINT ( 'NONE', #12558 ) ;
#240862=ORIENTED_EDGE ( 'NONE', *, *, #244775, .F. ) ;
#240918=CARTESIAN_POINT ( 'NONE',  ( -12.26136940704871670, 48.33137198101100296, -234.0751437313343502 ) ) ;
#241053=DIRECTION ( 'NONE',  ( -1.020425574104004394E-15, -0.9126074666063769270, -0.4088369013363280513 ) ) ;
#241055=EDGE_LOOP ( 'NONE', ( #207743, #210917, #203213, #118868, #18687 ) ) ;
#241194=CARTESIAN_POINT ( 'NONE',  ( -16.92973740335347443, 51.65264569848611842, -231.8847607149625958 ) ) ;
#241206=LINE ( 'NONE', #221595, #203460 ) ;
#241313=PLANE ( 'NONE',  #85584 ) ;
#241343=PLANE ( 'NONE',  #193370 ) ;
#241677=SURFACE_STYLE_USAGE ( .BOTH. , #4332 ) ;
#241807=ORIENTED_EDGE ( 'NONE', *, *, #86351, .F. ) ;
#241866=EDGE_CURVE ( 'NONE', #201957, #51518, #63939, .T. ) ;
#242002=CARTESIAN_POINT ( 'NONE',  ( -16.87435696428308063, 44.13547318391088936, -235.2989327256209151 ) ) ;
#242306=DIRECTION ( 'NONE',  ( 0.7071067811864931718, -0.2890913453341744099, 0.6453109281989217738 ) ) ;
#242363=CARTESIAN_POINT ( 'NONE',  ( 12.25000000000000000, 48.12247445990688277, -234.1702647910923361 ) ) ;
#242589=EDGE_CURVE ( 'NONE', #12028, #2285, #16743, .T. ) ;
#242695=AXIS2_PLACEMENT_3D ( 'NONE', #76664, #175796, #213609 ) ;
#242846=PRODUCT_DEFINITION_SHAPE ( 'NONE', 'NONE',  #148835 ) ;
#243173=ORIENTED_EDGE ( 'NONE', *, *, #137075, .F. ) ;
#243278=CARTESIAN_POINT ( 'NONE',  ( -16.92209698673566010, 44.19081817725273709, -235.2741415492630495 ) ) ;
#243437=PRODUCT_DEFINITION_CONTEXT ( 'detailed design', #69159, 'design' ) ;
#243493=ADVANCED_FACE ( 'NONE', ( #108744 ), #64549, .T. ) ;
#243531=CARTESIAN_POINT ( 'NONE',  ( -18.40000000000000213, 54.09347887257330711, -229.1540424707546322 ) ) ;
#243538=EDGE_CURVE ( 'NONE', #50660, #151483, #17046, .T. ) ;
#243554=PLANE ( 'NONE',  #251518 ) ;
#243741=CARTESIAN_POINT ( 'NONE',  ( -16.92778301347303582, 51.66969098184829079, -231.8678752041996347 ) ) ;
#243788=VERTEX_POINT ( 'NONE', #43019 ) ;
#243910=CARTESIAN_POINT ( 'NONE',  ( 18.54999999999999716, 51.61886293219128419, -231.9464690156495408 ) ) ;
#244056=CARTESIAN_POINT ( 'NONE',  ( -16.97048326478265423, 44.58366951172476433, -235.0981489915114082 ) ) ;
#244124=ORIENTED_EDGE ( 'NONE', *, *, #196871, .T. ) ;
#244549=LINE ( 'NONE', #104999, #193340 ) ;
#244775=EDGE_CURVE ( 'NONE', #150070, #244889, #91787, .T. ) ;
#244796=CARTESIAN_POINT ( 'NONE',  ( -16.97683809663752186, 44.82209472663103611, -234.9913374327310578 ) ) ;
#244811=CARTESIAN_POINT ( 'NONE',  ( -16.79139129368505579, 44.15602412204730598, -235.2952688487417277 ) ) ;
#244889=VERTEX_POINT ( 'NONE', #176480 ) ;
#245204=VERTEX_POINT ( 'NONE', #234851 ) ;
#245364=CARTESIAN_POINT ( 'NONE',  ( -16.94225986326249966, 44.40627002368546528, -235.1776217765174977 ) ) ;
#245435=CARTESIAN_POINT ( 'NONE',  ( -17.78043020864320667, 53.36034707231080887, -230.1761842539149256 ) ) ;
#245651=CARTESIAN_POINT ( 'NONE',  ( 13.99999999999999822, 47.91805600923871822, -233.7139610577891631 ) ) ;
#245700=VECTOR ( 'NONE', #11812, 1000.000000000000114 ) ;
#246256=CARTESIAN_POINT ( 'NONE',  ( -21.65000000000000213, 45.23934133962703186, -237.7629717664446787 ) ) ;
#246325=DIRECTION ( 'NONE',  ( 0.000000000000000000, -0.4088369013363281068, 0.9126074666063770380 ) ) ;
#246374=CARTESIAN_POINT ( 'NONE',  ( -16.94445028196807002, 51.64060657411747712, -231.8906364537310196 ) ) ;
#246549=ORIENTED_EDGE ( 'NONE', *, *, #129180, .T. ) ;
#246882=VERTEX_POINT ( 'NONE', #199772 ) ;
#247132=ORIENTED_EDGE ( 'NONE', *, *, #155569, .F. ) ;
#247226=CARTESIAN_POINT ( 'NONE',  ( 18.39999999999999503, 54.09900352584866567, -229.1663746252470446 ) ) ;
#247316=DIRECTION ( 'NONE',  ( 1.000000000000000000, 0.000000000000000000, -0.000000000000000000 ) ) ;
#247354=CARTESIAN_POINT ( 'NONE',  ( -16.93302609847409457, 44.05834383477297678, -235.2823355200077344 ) ) ;
#247485=DIRECTION ( 'NONE',  ( -1.000000000000000000, -9.792504721693619684E-16, -4.386921467590155985E-16 ) ) ;
#247486=EDGE_LOOP ( 'NONE', ( #142323, #147875, #31564, #93528, #168693 ) ) ;
#247882=CARTESIAN_POINT ( 'NONE',  ( -21.64999999999999858, 44.18585876254595490, -235.1667871698132046 ) ) ;
#247953=CARTESIAN_POINT ( 'NONE',  ( -18.40000000000000213, 54.09347887257330711, -229.1540424707546322 ) ) ;
#248260=CARTESIAN_POINT ( 'NONE',  ( -17.73285935862988083, 41.56619374751048213, -235.4550095799147016 ) ) ;
#248405=ADVANCED_FACE ( 'NONE', ( #94275 ), #212953, .F. ) ;
#248443=DIRECTION ( 'NONE',  ( 0.000000000000000000, -0.9126074666063660468, -0.4088369013363524762 ) ) ;
#248642=CARTESIAN_POINT ( 'NONE',  ( -17.73285935861977691, 53.44571795644451129, -230.1331290949856054 ) ) ;
#248676=VERTEX_POINT ( 'NONE', #231903 ) ;
#248678=EDGE_CURVE ( 'NONE', #2285, #69236, #233196, .T. ) ;
#248804=DIRECTION ( 'NONE',  ( 1.000000000000000000, 0.000000000000000000, 0.000000000000000000 ) ) ;
#249058=ORIENTED_EDGE ( 'NONE', *, *, #78141, .F. ) ;
#249195=ORIENTED_EDGE ( 'NONE', *, *, #132905, .F. ) ;
#249342=DIRECTION ( 'NONE',  ( 0.000000000000000000, -0.9126074666063769270, -0.4088369013363280513 ) ) ;
#249642=PRESENTATION_STYLE_ASSIGNMENT (( #133533 ) ) ;
#249796=CARTESIAN_POINT ( 'NONE',  ( -16.87786941232801041, 51.64033894800659397, -231.9279124044847151 ) ) ;
#249830=FACE_OUTER_BOUND ( 'NONE', #21193, .T. ) ;
#249935=CARTESIAN_POINT ( 'NONE',  ( -16.93339986808596720, 44.03628838426681824, -235.2829882368675101 ) ) ;
#249947=CARTESIAN_POINT ( 'NONE',  ( -16.77308656112214891, 44.13565801420894985, -235.2988526227105410 ) ) ;
#250045=VECTOR ( 'NONE', #44745, 1000.000000000000000 ) ;
#250055=CARTESIAN_POINT ( 'NONE',  ( -16.97683809663752186, 50.97313360171293084, -232.3453239361865315 ) ) ;
#250221=CYLINDRICAL_SURFACE ( 'NONE', #210443, 0.9000000000000014655 ) ;
#250412=CARTESIAN_POINT ( 'NONE',  ( -16.98495255085918032, 44.09872649034048209, -235.2545122050661064 ) ) ;
#250415=ADVANCED_FACE ( 'NONE', ( #182509 ), #72974, .T. ) ;
#250925=CYLINDRICAL_SURFACE ( 'NONE', #16139, 0.9000000000000014655 ) ;
#251032=CARTESIAN_POINT ( 'NONE',  ( 15.39793903038207645, 47.12322829752086761, -234.5744283691288388 ) ) ;
#251120=ORIENTED_EDGE ( 'NONE', *, *, #13334, .F. ) ;
#251160=LINE ( 'NONE', #132526, #180313 ) ;
#251163=ORIENTED_EDGE ( 'NONE', *, *, #208918, .T. ) ;
#251174=ORIENTED_EDGE ( 'NONE', *, *, #94110, .F. ) ;
#251197=CARTESIAN_POINT ( 'NONE',  ( -16.93583594267724379, 44.02882368590770312, -235.2824757905454760 ) ) ;
#251393=CARTESIAN_POINT ( 'NONE',  ( -16.86578989773641979, 44.01660614304713448, -235.3140431590063031 ) ) ;
#251438=ADVANCED_FACE ( 'NONE', ( #97820 ), #216515, .F. ) ;
#251476=VERTEX_POINT ( 'NONE', #54856 ) ;
#251518=AXIS2_PLACEMENT_3D ( 'NONE', #23260, #182321, #25794 ) ;
#251818=DIRECTION ( 'NONE',  ( 1.020425574104004394E-15, 0.9126074666063770380, 0.4088369013363281068 ) ) ;
#252317=CARTESIAN_POINT ( 'NONE',  ( 13.12220780326571834, 46.70395665056641832, -234.7173882531050140 ) ) ;
#252422=CARTESIAN_POINT ( 'NONE',  ( -16.87683809663752044, 50.93224991157929082, -232.2540631895258798 ) ) ;
#252483=CARTESIAN_POINT ( 'NONE',  ( -16.94037747912386394, 44.01927583580262393, -235.2813664045062865 ) ) ;
#252655=DIRECTION ( 'NONE',  ( -0.000000000000000000, 0.9126074666063770380, 0.4088369013363281068 ) ) ;
#252760=( BOUNDED_CURVE ( )  B_SPLINE_CURVE ( 3, ( #42210, #40949, #80007, #63035 ),
 .UNSPECIFIED., .F., .F. ) 
 B_SPLINE_CURVE_WITH_KNOTS ( ( 4, 4 ),
 ( 3.432212674861196522, 3.693332928900582068 ),
 .UNSPECIFIED. ) 
 CURVE ( )  GEOMETRIC_REPRESENTATION_ITEM ( )  RATIONAL_B_SPLINE_CURVE ( ( 1.000000000000000000, 0.9943260843901261525, 0.9943260843901261525, 1.000000000000000000 ) ) 
 REPRESENTATION_ITEM ( '' )  );
#252885=CARTESIAN_POINT ( 'NONE',  ( 21.13736287352038445, 41.81077915253129618, -238.4259954500851109 ) ) ;
#252892=CARTESIAN_POINT ( 'NONE',  ( -16.93826681692523195, 51.68086471459877629, -231.8513817628493712 ) ) ;
#253173=ORIENTED_EDGE ( 'NONE', *, *, #232325, .F. ) ;
#253343=FACE_OUTER_BOUND ( 'NONE', #77176, .T. ) ;
#253436=ORIENTED_EDGE ( 'NONE', *, *, #150906, .F. ) ;
#253600=CARTESIAN_POINT ( 'NONE',  ( 12.84233041328156766, 46.89553527312528303, -234.6535825622730158 ) ) ;
#253618=LINE ( 'NONE', #75038, #115755 ) ;
#253621=CARTESIAN_POINT ( 'NONE',  ( -17.11825945287481332, 51.57797924205760864, -231.8552082689889460 ) ) ;
#254333=CARTESIAN_POINT ( 'NONE',  ( -18.34804628011471195, 40.40989152675304297, -235.2989281452920807 ) ) ;
#254380=CARTESIAN_POINT ( 'NONE',  ( -16.86445178670659217, 44.09327534691641404, -235.3044585041410244 ) ) ;
#254503=CARTESIAN_POINT ( 'NONE',  ( 16.87683809663750267, 44.13548170601895038, -235.2989316066074821 ) ) ;
#254699=EDGE_CURVE ( 'NONE', #248676, #14789, #117862, .T. ) ;
#254839=CARTESIAN_POINT ( 'NONE',  ( 13.76927104934457979, 46.49260333018392544, -234.7842902611276941 ) ) ;
#255182=CARTESIAN_POINT ( 'NONE',  ( 23.24999999999999645, 40.29670989715187090, -235.0462836312595130 ) ) ;
#255252=CARTESIAN_POINT ( 'NONE',  ( -13.88555196119802915, 46.48141361689234685, -234.7877205119061728 ) ) ;
#255327=ORIENTED_EDGE ( 'NONE', *, *, #146606, .T. ) ;
#255540=CARTESIAN_POINT ( 'NONE',  ( 18.39999999999999503, 53.98582189624753624, -228.9137301112145622 ) ) ;
#255615=CARTESIAN_POINT ( 'NONE',  ( -14.00000000000000178, 47.91805600923872532, -233.7139610577891631 ) ) ;
#255662=CARTESIAN_POINT ( 'NONE',  ( -16.96982749440684657, 44.56876802688330486, -235.1048246731278084 ) ) ;
#255770=VECTOR ( 'NONE', #55860, 1000.000000000000114 ) ;
#255806=AXIS2_PLACEMENT_3D ( 'NONE', #131052, #170239, #248443 ) ;
#255836=DIRECTION ( 'NONE',  ( 1.000000000000000000, 0.000000000000000000, 0.000000000000000000 ) ) ;
#255908=COLOUR_RGB ( '', 0.72549020, 0.75294118, 0.79215686) ;
#256217=CARTESIAN_POINT ( 'NONE',  ( -16.89935556175725395, 51.17198062720201790, -232.1466667825101808 ) ) ;
#256338=ORIENTED_EDGE ( 'NONE', *, *, #213326, .T. ) ;
#256433=ORIENTED_EDGE ( 'NONE', *, *, #9065, .T. ) ;
#256489=CARTESIAN_POINT ( 'NONE',  ( -23.25000000000000355, 40.29670989715187090, -235.0462836312595130 ) ) ;
#256531=CARTESIAN_POINT ( 'NONE',  ( -12.60206096961792355, 47.12322829752087472, -234.5744283691289240 ) ) ;
#256571=CARTESIAN_POINT ( 'NONE',  ( -12.68215100488889924, 49.15934945732310268, -233.6546618023459985 ) ) ;
#256696=CARTESIAN_POINT ( 'NONE',  ( -16.93415306273742260, 51.65501928279542199, -231.8802803063003353 ) ) ;
#256835=ORIENTED_EDGE ( 'NONE', *, *, #128489, .F. ) ;
#256876=ORIENTED_EDGE ( 'NONE', *, *, #35886, .F. ) ;
#256912=CYLINDRICAL_SURFACE ( 'NONE', #213668, 14.30833333333333357 ) ;
#256962=ORIENTED_EDGE ( 'NONE', *, *, #91028, .T. ) ;
#257409=VECTOR ( 'NONE', #7798, 1000.000000000000114 ) ;
#257487=CARTESIAN_POINT ( 'NONE',  ( 15.73863059295127798, 48.33137198101099585, -234.0751437313343786 ) ) ;
#257518=VECTOR ( 'NONE', #164541, 1000.000000000000114 ) ;
#257820=CARTESIAN_POINT ( 'NONE',  ( -15.52965525596987995, 47.30882569885145017, -234.5067857460875302 ) ) ;
#257848=VECTOR ( 'NONE', #31334, 1000.000000000000114 ) ;
#257857=CARTESIAN_POINT ( 'NONE',  ( -14.11361717019516249, 49.67565583792541162, -233.3567449137543974 ) ) ;
ENDSEC;
END-ISO-10303-21;
